ISO-10303-21;
HEADER;
/* Generated by software containing ST-Developer
 * from STEP Tools, Inc. (www.steptools.com) 
 */

FILE_DESCRIPTION(
/* description */ ('Hand wheel with handle and shaft collar'),
/* implementation_level */ '2;1');

FILE_NAME(
/* name */ 'Cage (1).step',
/* time_stamp */ '2026-10-28T03:23:19-07:00',
/* author */ (''),
/* organization */ (''),
/* preprocessor_version */ 'ST-DEVELOPER v20.2',
/* originating_system */ 'Autodesk Translation Framework v15.17.0.0',
/* authorisation */ '');

FILE_SCHEMA (('AUTOMOTIVE_DESIGN { 1 0 10303 214 3 1 1 }'));
ENDSEC;

DATA;
#10=MECHANICAL_DESIGN_GEOMETRIC_PRESENTATION_REPRESENTATION('',(#436),#10510);
#249=B_SPLINE_CURVE_WITH_KNOTS('',3,(#9803,#9804,#9805,#9806,#9807,#9808,
#9809,#9810,#9811,#9812,#9813,#9814,#9815,#9816,#9817,#9818,#9819,#9820,
#9821,#9822,#9823,#9824),.UNSPECIFIED.,.F.,.F.,(4,2,2,2,2,2,2,2,2,2,4),
(0.0473477652366656,0.126350602536658,0.189525903804987,0.252701205073317,
0.313298422430275,0.373895639787233,0.434492857144191,0.495090074501149,
0.558265375769478,0.621440677037807,0.7004435143378),.UNSPECIFIED.);
#250=B_SPLINE_CURVE_WITH_KNOTS('',3,(#9828,#9829,#9830,#9831,#9832,#9833,
#9834,#9835,#9836,#9837,#9838,#9839,#9840,#9841,#9842,#9843,#9844,#9845,
#9846,#9847,#9848,#9849),.UNSPECIFIED.,.F.,.F.,(4,2,2,2,2,2,2,2,2,2,4),
(0.0464897534940957,0.0852567806515119,0.170513561303024,0.246687263103517,
0.308657850341199,0.370628437578881,0.432599024816563,0.494569612054245,
0.570743313854739,0.656000094506251,0.694767121663666),.UNSPECIFIED.);
#251=B_SPLINE_CURVE_WITH_KNOTS('',3,(#9855,#9856,#9857,#9858,#9859,#9860,
#9861,#9862,#9863,#9864,#9865,#9866,#9867,#9868,#9869,#9870,#9871,#9872,
#9873,#9874,#9875,#9876),.UNSPECIFIED.,.F.,.F.,(4,2,2,2,2,2,2,2,2,2,4),
(0.0464897534940957,0.0852567806515118,0.170513561303024,0.246687263103517,
0.308657850341199,0.370628437578881,0.432599024816563,0.494569612054245,
0.570743313854738,0.65600009450625,0.694767121663666),.UNSPECIFIED.);
#252=B_SPLINE_CURVE_WITH_KNOTS('',3,(#9880,#9881,#9882,#9883,#9884,#9885,
#9886,#9887,#9888,#9889,#9890,#9891,#9892,#9893,#9894,#9895,#9896,#9897,
#9898,#9899,#9900,#9901),.UNSPECIFIED.,.F.,.F.,(4,2,2,2,2,2,2,2,2,2,4),
(0.0464897534940957,0.0852567806515119,0.170513561303024,0.246687263103517,
0.308657850341199,0.370628437578881,0.432599024816563,0.494569612054245,
0.570743313854739,0.656000094506251,0.694767121663666),.UNSPECIFIED.);
#253=B_SPLINE_CURVE_WITH_KNOTS('',3,(#9905,#9906,#9907,#9908,#9909,#9910,
#9911,#9912,#9913,#9914,#9915,#9916),.UNSPECIFIED.,.F.,.F.,(4,2,2,2,2,4),
(0.0464897534940957,0.0852567806515119,0.170513561303024,0.246687263103517,
0.308657850341199,0.370628437578881),.UNSPECIFIED.);
#254=B_SPLINE_CURVE_WITH_KNOTS('',3,(#9921,#9922,#9923,#9924,#9925,#9926,
#9927,#9928,#9929,#9930,#9931,#9932),.UNSPECIFIED.,.F.,.F.,(4,2,2,2,2,4),
(0.370628437578881,0.432599024816563,0.494569612054245,0.570743313854738,
0.65600009450625,0.694767121663666),.UNSPECIFIED.);
#255=B_SPLINE_CURVE_WITH_KNOTS('',3,(#9936,#9937,#9938,#9939,#9940,#9941,
#9942,#9943,#9944,#9945,#9946,#9947,#9948,#9949,#9950,#9951,#9952,#9953,
#9954,#9955,#9956,#9957),.UNSPECIFIED.,.F.,.F.,(4,2,2,2,2,2,2,2,2,2,4),
(0.0464897534940957,0.0852567806515121,0.170513561303024,0.246687263103518,
0.308657850341199,0.370628437578881,0.432599024816563,0.494569612054245,
0.570743313854738,0.65600009450625,0.694767121663666),.UNSPECIFIED.);
#256=B_SPLINE_CURVE_WITH_KNOTS('',3,(#9961,#9962,#9963,#9964,#9965,#9966,
#9967,#9968,#9969,#9970,#9971,#9972,#9973,#9974,#9975,#9976,#9977,#9978,
#9979,#9980,#9981,#9982),.UNSPECIFIED.,.F.,.F.,(4,2,2,2,2,2,2,2,2,2,4),
(0.0464897534940957,0.0852567806515119,0.170513561303024,0.246687263103517,
0.308657850341199,0.370628437578881,0.432599024816563,0.494569612054245,
0.570743313854738,0.65600009450625,0.694767121663667),.UNSPECIFIED.);
#257=B_SPLINE_CURVE_WITH_KNOTS('',3,(#9986,#9987,#9988,#9989,#9990,#9991,
#9992,#9993,#9994,#9995,#9996,#9997,#9998,#9999,#10000,#10001,#10002,#10003,
#10004,#10005,#10006,#10007),.UNSPECIFIED.,.F.,.F.,(4,2,2,2,2,2,2,2,2,2,
4),(0.0464897534940957,0.0852567806515119,0.170513561303024,0.246687263103517,
0.308657850341199,0.370628437578881,0.432599024816563,0.494569612054245,
0.570743313854738,0.65600009450625,0.694767121663666),.UNSPECIFIED.);
#258=B_SPLINE_CURVE_WITH_KNOTS('',3,(#10011,#10012,#10013,#10014,#10015,
#10016,#10017,#10018,#10019,#10020,#10021,#10022,#10023,#10024,#10025,#10026,
#10027,#10028,#10029,#10030,#10031,#10032),.UNSPECIFIED.,.F.,.F.,(4,2,2,
2,2,2,2,2,2,2,4),(0.0464897534940957,0.0852567806515119,0.170513561303024,
0.246687263103517,0.308657850341199,0.370628437578881,0.432599024816563,
0.494569612054245,0.570743313854739,0.656000094506251,0.694767121663667),
 .UNSPECIFIED.);
#259=B_SPLINE_CURVE_WITH_KNOTS('',3,(#10040,#10041,#10042,#10043,#10044,
#10045,#10046,#10047,#10048,#10049,#10050,#10051,#10052,#10053,#10054,#10055,
#10056,#10057,#10058,#10059,#10060,#10061),.UNSPECIFIED.,.F.,.F.,(4,2,2,
2,2,2,2,2,2,2,4),(0.0473477652366656,0.126350602536658,0.189525903804987,
0.252701205073316,0.313298422430274,0.373895639787232,0.434492857144191,
0.495090074501149,0.558265375769478,0.621440677037807,0.7004435143378),
 .UNSPECIFIED.);
#260=B_SPLINE_CURVE_WITH_KNOTS('',3,(#10069,#10070,#10071,#10072,#10073,
#10074,#10075,#10076,#10077,#10078,#10079,#10080,#10081,#10082,#10083,#10084,
#10085,#10086,#10087,#10088,#10089,#10090),.UNSPECIFIED.,.F.,.F.,(4,2,2,
2,2,2,2,2,2,2,4),(0.0473477652366656,0.126350602536658,0.189525903804987,
0.252701205073317,0.313298422430275,0.373895639787233,0.434492857144191,
0.495090074501149,0.558265375769478,0.621440677037807,0.7004435143378),
 .UNSPECIFIED.);
#261=B_SPLINE_CURVE_WITH_KNOTS('',3,(#10099,#10100,#10101,#10102,#10103,
#10104,#10105,#10106,#10107,#10108,#10109,#10110),.UNSPECIFIED.,.F.,.F.,
(4,2,2,2,2,4),(0.0473477652366656,0.126350602536658,0.189525903804987,0.252701205073316,
0.313298422430275,0.373895639787233),.UNSPECIFIED.);
#262=B_SPLINE_CURVE_WITH_KNOTS('',3,(#10112,#10113,#10114,#10115,#10116,
#10117,#10118,#10119,#10120,#10121,#10122,#10123),.UNSPECIFIED.,.F.,.F.,
(4,2,2,2,2,4),(0.373895639787233,0.434492857144191,0.495090074501149,0.558265375769478,
0.621440677037807,0.7004435143378),.UNSPECIFIED.);
#263=B_SPLINE_CURVE_WITH_KNOTS('',3,(#10130,#10131,#10132,#10133,#10134,
#10135,#10136,#10137,#10138,#10139,#10140,#10141,#10142,#10143,#10144,#10145,
#10146,#10147,#10148,#10149,#10150,#10151),.UNSPECIFIED.,.F.,.F.,(4,2,2,
2,2,2,2,2,2,2,4),(0.0473477652366656,0.126350602536658,0.189525903804987,
0.252701205073316,0.313298422430275,0.373895639787233,0.434492857144191,
0.495090074501149,0.558265375769478,0.621440677037807,0.7004435143378),
 .UNSPECIFIED.);
#264=B_SPLINE_CURVE_WITH_KNOTS('',3,(#10159,#10160,#10161,#10162,#10163,
#10164,#10165,#10166,#10167,#10168,#10169,#10170,#10171,#10172,#10173,#10174,
#10175,#10176,#10177,#10178,#10179,#10180),.UNSPECIFIED.,.F.,.F.,(4,2,2,
2,2,2,2,2,2,2,4),(0.0473477652366656,0.126350602536658,0.189525903804987,
0.252701205073317,0.313298422430275,0.373895639787233,0.434492857144191,
0.495090074501149,0.558265375769478,0.621440677037807,0.7004435143378),
 .UNSPECIFIED.);
#265=B_SPLINE_CURVE_WITH_KNOTS('',3,(#10188,#10189,#10190,#10191,#10192,
#10193,#10194,#10195,#10196,#10197,#10198,#10199,#10200,#10201,#10202,#10203,
#10204,#10205,#10206,#10207,#10208,#10209),.UNSPECIFIED.,.F.,.F.,(4,2,2,
2,2,2,2,2,2,2,4),(0.0473477652366656,0.126350602536658,0.189525903804987,
0.252701205073316,0.313298422430275,0.373895639787233,0.434492857144191,
0.495090074501149,0.558265375769478,0.621440677037807,0.7004435143378),
 .UNSPECIFIED.);
#266=B_SPLINE_CURVE_WITH_KNOTS('',3,(#10218,#10219,#10220,#10221,#10222,
#10223,#10224,#10225,#10226,#10227,#10228,#10229,#10230,#10231,#10232,#10233,
#10234,#10235,#10236,#10237,#10238,#10239),.UNSPECIFIED.,.F.,.F.,(4,2,2,
2,2,2,2,2,2,2,4),(0.0473477652366656,0.126350602536658,0.189525903804987,
0.252701205073317,0.313298422430275,0.373895639787233,0.434492857144191,
0.495090074501149,0.558265375769478,0.621440677037807,0.7004435143378),
 .UNSPECIFIED.);
#289=SPHERICAL_SURFACE('',#6251,0.247676);
#290=SPHERICAL_SURFACE('',#6267,0.247676);
#291=SPHERICAL_SURFACE('',#6272,0.247676);
#292=SPHERICAL_SURFACE('',#6277,0.247676);
#293=SPHERICAL_SURFACE('',#6282,0.247676);
#294=SPHERICAL_SURFACE('',#6287,0.247676);
#295=SPHERICAL_SURFACE('',#6292,0.247676);
#296=SPHERICAL_SURFACE('',#6300,0.247676);
#358=SHAPE_REPRESENTATION_RELATIONSHIP('SRR','None',#10677,#390);
#390=ADVANCED_BREP_SHAPE_REPRESENTATION('',(#481),#10504);
#436=STYLED_ITEM('',(#10908),#481);
#481=MANIFOLD_SOLID_BREP('Continuous crown cage',#5337);
#587=FACE_BOUND('',#1466,.T.);
#734=PLANE('',#6264);
#735=PLANE('',#6269);
#736=PLANE('',#6274);
#737=PLANE('',#6279);
#738=PLANE('',#6284);
#739=PLANE('',#6289);
#740=PLANE('',#6298);
#741=PLANE('',#6302);
#742=PLANE('',#6303);
#1028=FACE_OUTER_BOUND('',#1448,.T.);
#1029=FACE_OUTER_BOUND('',#1449,.T.);
#1030=FACE_OUTER_BOUND('',#1450,.T.);
#1031=FACE_OUTER_BOUND('',#1451,.T.);
#1032=FACE_OUTER_BOUND('',#1452,.T.);
#1033=FACE_OUTER_BOUND('',#1453,.T.);
#1034=FACE_OUTER_BOUND('',#1454,.T.);
#1035=FACE_OUTER_BOUND('',#1455,.T.);
#1036=FACE_OUTER_BOUND('',#1456,.T.);
#1037=FACE_OUTER_BOUND('',#1457,.T.);
#1038=FACE_OUTER_BOUND('',#1458,.T.);
#1039=FACE_OUTER_BOUND('',#1459,.T.);
#1040=FACE_OUTER_BOUND('',#1460,.T.);
#1041=FACE_OUTER_BOUND('',#1461,.T.);
#1042=FACE_OUTER_BOUND('',#1462,.T.);
#1043=FACE_OUTER_BOUND('',#1463,.T.);
#1044=FACE_OUTER_BOUND('',#1464,.T.);
#1045=FACE_OUTER_BOUND('',#1465,.T.);
#1046=FACE_OUTER_BOUND('',#1467,.T.);
#1448=EDGE_LOOP('',(#4653,#4654,#4655,#4656));
#1449=EDGE_LOOP('',(#4657,#4658,#4659,#4660,#4661,#4662,#4663,#4664,#4665,
#4666,#4667,#4668,#4669,#4670,#4671,#4672,#4673,#4674,#4675,#4676));
#1450=EDGE_LOOP('',(#4677,#4678,#4679,#4680));
#1451=EDGE_LOOP('',(#4681,#4682,#4683,#4684));
#1452=EDGE_LOOP('',(#4685,#4686,#4687,#4688));
#1453=EDGE_LOOP('',(#4689,#4690,#4691,#4692));
#1454=EDGE_LOOP('',(#4693,#4694,#4695,#4696));
#1455=EDGE_LOOP('',(#4697,#4698,#4699,#4700,#4701,#4702));
#1456=EDGE_LOOP('',(#4703,#4704,#4705,#4706));
#1457=EDGE_LOOP('',(#4707,#4708,#4709,#4710));
#1458=EDGE_LOOP('',(#4711,#4712,#4713,#4714));
#1459=EDGE_LOOP('',(#4715,#4716,#4717,#4718));
#1460=EDGE_LOOP('',(#4719,#4720,#4721,#4722));
#1461=EDGE_LOOP('',(#4723,#4724,#4725,#4726));
#1462=EDGE_LOOP('',(#4727,#4728,#4729,#4730,#4731,#4732,#4733,#4734,#4735,
#4736,#4737,#4738,#4739,#4740,#4741,#4742,#4743,#4744,#4745,#4746));
#1463=EDGE_LOOP('',(#4747,#4748,#4749,#4750));
#1464=EDGE_LOOP('',(#4751,#4752,#4753,#4754));
#1465=EDGE_LOOP('',(#4755));
#1466=EDGE_LOOP('',(#4756));
#1467=EDGE_LOOP('',(#4757,#4758,#4759,#4760));
#1788=LINE('',#9918,#2098);
#1789=LINE('',#10214,#2099);
#2098=VECTOR('',#7816,1.019052);
#2099=VECTOR('',#7893,0.980948);
#2384=CIRCLE('',#6252,0.243053047864041);
#2385=CIRCLE('',#6253,0.243053047864041);
#2386=CIRCLE('',#6255,1.019052);
#2387=CIRCLE('',#6256,1.019052);
#2388=CIRCLE('',#6257,1.019052);
#2389=CIRCLE('',#6258,1.019052);
#2390=CIRCLE('',#6259,1.019052);
#2391=CIRCLE('',#6260,1.019052);
#2392=CIRCLE('',#6261,1.019052);
#2393=CIRCLE('',#6262,1.019052);
#2394=CIRCLE('',#6263,1.019052);
#2395=CIRCLE('',#6265,0.980948);
#2396=CIRCLE('',#6266,0.243053047864041);
#2397=CIRCLE('',#6268,0.243053047864041);
#2398=CIRCLE('',#6270,0.980948);
#2399=CIRCLE('',#6271,0.243053047864041);
#2400=CIRCLE('',#6273,0.243053047864041);
#2401=CIRCLE('',#6275,0.980948);
#2402=CIRCLE('',#6276,0.243053047864041);
#2403=CIRCLE('',#6278,0.243053047864041);
#2404=CIRCLE('',#6280,0.980948);
#2405=CIRCLE('',#6281,0.243053047864041);
#2406=CIRCLE('',#6283,0.243053047864041);
#2407=CIRCLE('',#6285,0.980948);
#2408=CIRCLE('',#6286,0.243053047864041);
#2409=CIRCLE('',#6288,0.243053047864041);
#2410=CIRCLE('',#6290,0.980948);
#2411=CIRCLE('',#6291,0.243053047864041);
#2412=CIRCLE('',#6293,0.243053047864041);
#2413=CIRCLE('',#6295,0.980948);
#2414=CIRCLE('',#6296,0.980948);
#2415=CIRCLE('',#6297,0.980948);
#2416=CIRCLE('',#6299,0.243053047864041);
#2417=CIRCLE('',#6301,0.243053047864041);
#2822=VERTEX_POINT('',#9801);
#2823=VERTEX_POINT('',#9802);
#2824=VERTEX_POINT('',#9825);
#2825=VERTEX_POINT('',#9827);
#2826=VERTEX_POINT('',#9852);
#2827=VERTEX_POINT('',#9854);
#2828=VERTEX_POINT('',#9877);
#2829=VERTEX_POINT('',#9879);
#2830=VERTEX_POINT('',#9902);
#2831=VERTEX_POINT('',#9904);
#2832=VERTEX_POINT('',#9917);
#2833=VERTEX_POINT('',#9920);
#2834=VERTEX_POINT('',#9933);
#2835=VERTEX_POINT('',#9935);
#2836=VERTEX_POINT('',#9958);
#2837=VERTEX_POINT('',#9960);
#2838=VERTEX_POINT('',#9983);
#2839=VERTEX_POINT('',#9985);
#2840=VERTEX_POINT('',#10008);
#2841=VERTEX_POINT('',#10010);
#2842=VERTEX_POINT('',#10035);
#2843=VERTEX_POINT('',#10039);
#2844=VERTEX_POINT('',#10064);
#2845=VERTEX_POINT('',#10068);
#2846=VERTEX_POINT('',#10093);
#2847=VERTEX_POINT('',#10097);
#2848=VERTEX_POINT('',#10098);
#2849=VERTEX_POINT('',#10125);
#2850=VERTEX_POINT('',#10129);
#2851=VERTEX_POINT('',#10154);
#2852=VERTEX_POINT('',#10158);
#2853=VERTEX_POINT('',#10183);
#2854=VERTEX_POINT('',#10187);
#2855=VERTEX_POINT('',#10212);
#2856=VERTEX_POINT('',#10215);
#2857=VERTEX_POINT('',#10217);
#3444=EDGE_CURVE('',#2822,#2823,#249,.T.);
#3445=EDGE_CURVE('',#2824,#2822,#2384,.T.);
#3446=EDGE_CURVE('',#2825,#2824,#250,.T.);
#3447=EDGE_CURVE('',#2823,#2825,#2385,.T.);
#3448=EDGE_CURVE('',#2826,#2824,#2386,.T.);
#3449=EDGE_CURVE('',#2826,#2827,#251,.T.);
#3450=EDGE_CURVE('',#2828,#2827,#2387,.T.);
#3451=EDGE_CURVE('',#2828,#2829,#252,.T.);
#3452=EDGE_CURVE('',#2830,#2829,#2388,.T.);
#3453=EDGE_CURVE('',#2830,#2831,#253,.T.);
#3454=EDGE_CURVE('',#2831,#2832,#1788,.T.);
#3455=EDGE_CURVE('',#2832,#2832,#2389,.T.);
#3456=EDGE_CURVE('',#2831,#2833,#254,.T.);
#3457=EDGE_CURVE('',#2834,#2833,#2390,.T.);
#3458=EDGE_CURVE('',#2834,#2835,#255,.T.);
#3459=EDGE_CURVE('',#2836,#2835,#2391,.T.);
#3460=EDGE_CURVE('',#2836,#2837,#256,.T.);
#3461=EDGE_CURVE('',#2838,#2837,#2392,.T.);
#3462=EDGE_CURVE('',#2838,#2839,#257,.T.);
#3463=EDGE_CURVE('',#2840,#2839,#2393,.T.);
#3464=EDGE_CURVE('',#2840,#2841,#258,.T.);
#3465=EDGE_CURVE('',#2825,#2841,#2394,.T.);
#3466=EDGE_CURVE('',#2822,#2842,#2395,.T.);
#3467=EDGE_CURVE('',#2842,#2826,#2396,.T.);
#3468=EDGE_CURVE('',#2843,#2842,#259,.T.);
#3469=EDGE_CURVE('',#2827,#2843,#2397,.T.);
#3470=EDGE_CURVE('',#2843,#2844,#2398,.T.);
#3471=EDGE_CURVE('',#2844,#2828,#2399,.T.);
#3472=EDGE_CURVE('',#2845,#2844,#260,.T.);
#3473=EDGE_CURVE('',#2829,#2845,#2400,.T.);
#3474=EDGE_CURVE('',#2845,#2846,#2401,.T.);
#3475=EDGE_CURVE('',#2846,#2830,#2402,.T.);
#3476=EDGE_CURVE('',#2847,#2848,#261,.T.);
#3477=EDGE_CURVE('',#2833,#2847,#2403,.T.);
#3478=EDGE_CURVE('',#2848,#2846,#262,.T.);
#3479=EDGE_CURVE('',#2847,#2849,#2404,.T.);
#3480=EDGE_CURVE('',#2849,#2834,#2405,.T.);
#3481=EDGE_CURVE('',#2850,#2849,#263,.T.);
#3482=EDGE_CURVE('',#2835,#2850,#2406,.T.);
#3483=EDGE_CURVE('',#2850,#2851,#2407,.T.);
#3484=EDGE_CURVE('',#2851,#2836,#2408,.T.);
#3485=EDGE_CURVE('',#2852,#2851,#264,.T.);
#3486=EDGE_CURVE('',#2837,#2852,#2409,.T.);
#3487=EDGE_CURVE('',#2852,#2853,#2410,.T.);
#3488=EDGE_CURVE('',#2853,#2838,#2411,.T.);
#3489=EDGE_CURVE('',#2854,#2853,#265,.T.);
#3490=EDGE_CURVE('',#2839,#2854,#2412,.T.);
#3491=EDGE_CURVE('',#2855,#2855,#2413,.T.);
#3492=EDGE_CURVE('',#2855,#2848,#1789,.T.);
#3493=EDGE_CURVE('',#2856,#2823,#2414,.T.);
#3494=EDGE_CURVE('',#2856,#2857,#266,.T.);
#3495=EDGE_CURVE('',#2854,#2857,#2415,.T.);
#3496=EDGE_CURVE('',#2841,#2856,#2416,.T.);
#3497=EDGE_CURVE('',#2857,#2840,#2417,.T.);
#4653=ORIENTED_EDGE('',*,*,#3444,.F.);
#4654=ORIENTED_EDGE('',*,*,#3445,.F.);
#4655=ORIENTED_EDGE('',*,*,#3446,.F.);
#4656=ORIENTED_EDGE('',*,*,#3447,.F.);
#4657=ORIENTED_EDGE('',*,*,#3446,.T.);
#4658=ORIENTED_EDGE('',*,*,#3448,.F.);
#4659=ORIENTED_EDGE('',*,*,#3449,.T.);
#4660=ORIENTED_EDGE('',*,*,#3450,.F.);
#4661=ORIENTED_EDGE('',*,*,#3451,.T.);
#4662=ORIENTED_EDGE('',*,*,#3452,.F.);
#4663=ORIENTED_EDGE('',*,*,#3453,.T.);
#4664=ORIENTED_EDGE('',*,*,#3454,.T.);
#4665=ORIENTED_EDGE('',*,*,#3455,.F.);
#4666=ORIENTED_EDGE('',*,*,#3454,.F.);
#4667=ORIENTED_EDGE('',*,*,#3456,.T.);
#4668=ORIENTED_EDGE('',*,*,#3457,.F.);
#4669=ORIENTED_EDGE('',*,*,#3458,.T.);
#4670=ORIENTED_EDGE('',*,*,#3459,.F.);
#4671=ORIENTED_EDGE('',*,*,#3460,.T.);
#4672=ORIENTED_EDGE('',*,*,#3461,.F.);
#4673=ORIENTED_EDGE('',*,*,#3462,.T.);
#4674=ORIENTED_EDGE('',*,*,#3463,.F.);
#4675=ORIENTED_EDGE('',*,*,#3464,.T.);
#4676=ORIENTED_EDGE('',*,*,#3465,.F.);
#4677=ORIENTED_EDGE('',*,*,#3445,.T.);
#4678=ORIENTED_EDGE('',*,*,#3466,.T.);
#4679=ORIENTED_EDGE('',*,*,#3467,.T.);
#4680=ORIENTED_EDGE('',*,*,#3448,.T.);
#4681=ORIENTED_EDGE('',*,*,#3468,.F.);
#4682=ORIENTED_EDGE('',*,*,#3469,.F.);
#4683=ORIENTED_EDGE('',*,*,#3449,.F.);
#4684=ORIENTED_EDGE('',*,*,#3467,.F.);
#4685=ORIENTED_EDGE('',*,*,#3469,.T.);
#4686=ORIENTED_EDGE('',*,*,#3470,.T.);
#4687=ORIENTED_EDGE('',*,*,#3471,.T.);
#4688=ORIENTED_EDGE('',*,*,#3450,.T.);
#4689=ORIENTED_EDGE('',*,*,#3472,.F.);
#4690=ORIENTED_EDGE('',*,*,#3473,.F.);
#4691=ORIENTED_EDGE('',*,*,#3451,.F.);
#4692=ORIENTED_EDGE('',*,*,#3471,.F.);
#4693=ORIENTED_EDGE('',*,*,#3473,.T.);
#4694=ORIENTED_EDGE('',*,*,#3474,.T.);
#4695=ORIENTED_EDGE('',*,*,#3475,.T.);
#4696=ORIENTED_EDGE('',*,*,#3452,.T.);
#4697=ORIENTED_EDGE('',*,*,#3476,.F.);
#4698=ORIENTED_EDGE('',*,*,#3477,.F.);
#4699=ORIENTED_EDGE('',*,*,#3456,.F.);
#4700=ORIENTED_EDGE('',*,*,#3453,.F.);
#4701=ORIENTED_EDGE('',*,*,#3475,.F.);
#4702=ORIENTED_EDGE('',*,*,#3478,.F.);
#4703=ORIENTED_EDGE('',*,*,#3477,.T.);
#4704=ORIENTED_EDGE('',*,*,#3479,.T.);
#4705=ORIENTED_EDGE('',*,*,#3480,.T.);
#4706=ORIENTED_EDGE('',*,*,#3457,.T.);
#4707=ORIENTED_EDGE('',*,*,#3481,.F.);
#4708=ORIENTED_EDGE('',*,*,#3482,.F.);
#4709=ORIENTED_EDGE('',*,*,#3458,.F.);
#4710=ORIENTED_EDGE('',*,*,#3480,.F.);
#4711=ORIENTED_EDGE('',*,*,#3482,.T.);
#4712=ORIENTED_EDGE('',*,*,#3483,.T.);
#4713=ORIENTED_EDGE('',*,*,#3484,.T.);
#4714=ORIENTED_EDGE('',*,*,#3459,.T.);
#4715=ORIENTED_EDGE('',*,*,#3485,.F.);
#4716=ORIENTED_EDGE('',*,*,#3486,.F.);
#4717=ORIENTED_EDGE('',*,*,#3460,.F.);
#4718=ORIENTED_EDGE('',*,*,#3484,.F.);
#4719=ORIENTED_EDGE('',*,*,#3486,.T.);
#4720=ORIENTED_EDGE('',*,*,#3487,.T.);
#4721=ORIENTED_EDGE('',*,*,#3488,.T.);
#4722=ORIENTED_EDGE('',*,*,#3461,.T.);
#4723=ORIENTED_EDGE('',*,*,#3462,.F.);
#4724=ORIENTED_EDGE('',*,*,#3488,.F.);
#4725=ORIENTED_EDGE('',*,*,#3489,.F.);
#4726=ORIENTED_EDGE('',*,*,#3490,.F.);
#4727=ORIENTED_EDGE('',*,*,#3491,.F.);
#4728=ORIENTED_EDGE('',*,*,#3492,.T.);
#4729=ORIENTED_EDGE('',*,*,#3478,.T.);
#4730=ORIENTED_EDGE('',*,*,#3474,.F.);
#4731=ORIENTED_EDGE('',*,*,#3472,.T.);
#4732=ORIENTED_EDGE('',*,*,#3470,.F.);
#4733=ORIENTED_EDGE('',*,*,#3468,.T.);
#4734=ORIENTED_EDGE('',*,*,#3466,.F.);
#4735=ORIENTED_EDGE('',*,*,#3444,.T.);
#4736=ORIENTED_EDGE('',*,*,#3493,.F.);
#4737=ORIENTED_EDGE('',*,*,#3494,.T.);
#4738=ORIENTED_EDGE('',*,*,#3495,.F.);
#4739=ORIENTED_EDGE('',*,*,#3489,.T.);
#4740=ORIENTED_EDGE('',*,*,#3487,.F.);
#4741=ORIENTED_EDGE('',*,*,#3485,.T.);
#4742=ORIENTED_EDGE('',*,*,#3483,.F.);
#4743=ORIENTED_EDGE('',*,*,#3481,.T.);
#4744=ORIENTED_EDGE('',*,*,#3479,.F.);
#4745=ORIENTED_EDGE('',*,*,#3476,.T.);
#4746=ORIENTED_EDGE('',*,*,#3492,.F.);
#4747=ORIENTED_EDGE('',*,*,#3447,.T.);
#4748=ORIENTED_EDGE('',*,*,#3465,.T.);
#4749=ORIENTED_EDGE('',*,*,#3496,.T.);
#4750=ORIENTED_EDGE('',*,*,#3493,.T.);
#4751=ORIENTED_EDGE('',*,*,#3464,.F.);
#4752=ORIENTED_EDGE('',*,*,#3497,.F.);
#4753=ORIENTED_EDGE('',*,*,#3494,.F.);
#4754=ORIENTED_EDGE('',*,*,#3496,.F.);
#4755=ORIENTED_EDGE('',*,*,#3455,.T.);
#4756=ORIENTED_EDGE('',*,*,#3491,.T.);
#4757=ORIENTED_EDGE('',*,*,#3490,.T.);
#4758=ORIENTED_EDGE('',*,*,#3495,.T.);
#4759=ORIENTED_EDGE('',*,*,#3497,.T.);
#4760=ORIENTED_EDGE('',*,*,#3463,.T.);
#4962=CYLINDRICAL_SURFACE('',#6254,1.019052);
#4963=CYLINDRICAL_SURFACE('',#6294,0.980948);
#5240=ADVANCED_FACE('',(#1028),#289,.F.);
#5241=ADVANCED_FACE('',(#1029),#4962,.T.);
#5242=ADVANCED_FACE('',(#1030),#734,.T.);
#5243=ADVANCED_FACE('',(#1031),#290,.F.);
#5244=ADVANCED_FACE('',(#1032),#735,.T.);
#5245=ADVANCED_FACE('',(#1033),#291,.F.);
#5246=ADVANCED_FACE('',(#1034),#736,.T.);
#5247=ADVANCED_FACE('',(#1035),#292,.F.);
#5248=ADVANCED_FACE('',(#1036),#737,.T.);
#5249=ADVANCED_FACE('',(#1037),#293,.F.);
#5250=ADVANCED_FACE('',(#1038),#738,.T.);
#5251=ADVANCED_FACE('',(#1039),#294,.F.);
#5252=ADVANCED_FACE('',(#1040),#739,.T.);
#5253=ADVANCED_FACE('',(#1041),#295,.F.);
#5254=ADVANCED_FACE('',(#1042),#4963,.F.);
#5255=ADVANCED_FACE('',(#1043),#740,.T.);
#5256=ADVANCED_FACE('',(#1044),#296,.F.);
#5257=ADVANCED_FACE('',(#1045,#587),#741,.T.);
#5258=ADVANCED_FACE('',(#1046),#742,.T.);
#5337=CLOSED_SHELL('',(#5240,#5241,#5242,#5243,#5244,#5245,#5246,#5247,
#5248,#5249,#5250,#5251,#5252,#5253,#5254,#5255,#5256,#5257,#5258));
#6250=AXIS2_PLACEMENT_3D('',#9799,#7800,#7801);
#6251=AXIS2_PLACEMENT_3D('',#9800,#7802,#7803);
#6252=AXIS2_PLACEMENT_3D('',#9826,#7804,#7805);
#6253=AXIS2_PLACEMENT_3D('',#9850,#7806,#7807);
#6254=AXIS2_PLACEMENT_3D('',#9851,#7808,#7809);
#6255=AXIS2_PLACEMENT_3D('',#9853,#7810,#7811);
#6256=AXIS2_PLACEMENT_3D('',#9878,#7812,#7813);
#6257=AXIS2_PLACEMENT_3D('',#9903,#7814,#7815);
#6258=AXIS2_PLACEMENT_3D('',#9919,#7817,#7818);
#6259=AXIS2_PLACEMENT_3D('',#9934,#7819,#7820);
#6260=AXIS2_PLACEMENT_3D('',#9959,#7821,#7822);
#6261=AXIS2_PLACEMENT_3D('',#9984,#7823,#7824);
#6262=AXIS2_PLACEMENT_3D('',#10009,#7825,#7826);
#6263=AXIS2_PLACEMENT_3D('',#10033,#7827,#7828);
#6264=AXIS2_PLACEMENT_3D('',#10034,#7829,#7830);
#6265=AXIS2_PLACEMENT_3D('',#10036,#7831,#7832);
#6266=AXIS2_PLACEMENT_3D('',#10037,#7833,#7834);
#6267=AXIS2_PLACEMENT_3D('',#10038,#7835,#7836);
#6268=AXIS2_PLACEMENT_3D('',#10062,#7837,#7838);
#6269=AXIS2_PLACEMENT_3D('',#10063,#7839,#7840);
#6270=AXIS2_PLACEMENT_3D('',#10065,#7841,#7842);
#6271=AXIS2_PLACEMENT_3D('',#10066,#7843,#7844);
#6272=AXIS2_PLACEMENT_3D('',#10067,#7845,#7846);
#6273=AXIS2_PLACEMENT_3D('',#10091,#7847,#7848);
#6274=AXIS2_PLACEMENT_3D('',#10092,#7849,#7850);
#6275=AXIS2_PLACEMENT_3D('',#10094,#7851,#7852);
#6276=AXIS2_PLACEMENT_3D('',#10095,#7853,#7854);
#6277=AXIS2_PLACEMENT_3D('',#10096,#7855,#7856);
#6278=AXIS2_PLACEMENT_3D('',#10111,#7857,#7858);
#6279=AXIS2_PLACEMENT_3D('',#10124,#7859,#7860);
#6280=AXIS2_PLACEMENT_3D('',#10126,#7861,#7862);
#6281=AXIS2_PLACEMENT_3D('',#10127,#7863,#7864);
#6282=AXIS2_PLACEMENT_3D('',#10128,#7865,#7866);
#6283=AXIS2_PLACEMENT_3D('',#10152,#7867,#7868);
#6284=AXIS2_PLACEMENT_3D('',#10153,#7869,#7870);
#6285=AXIS2_PLACEMENT_3D('',#10155,#7871,#7872);
#6286=AXIS2_PLACEMENT_3D('',#10156,#7873,#7874);
#6287=AXIS2_PLACEMENT_3D('',#10157,#7875,#7876);
#6288=AXIS2_PLACEMENT_3D('',#10181,#7877,#7878);
#6289=AXIS2_PLACEMENT_3D('',#10182,#7879,#7880);
#6290=AXIS2_PLACEMENT_3D('',#10184,#7881,#7882);
#6291=AXIS2_PLACEMENT_3D('',#10185,#7883,#7884);
#6292=AXIS2_PLACEMENT_3D('',#10186,#7885,#7886);
#6293=AXIS2_PLACEMENT_3D('',#10210,#7887,#7888);
#6294=AXIS2_PLACEMENT_3D('',#10211,#7889,#7890);
#6295=AXIS2_PLACEMENT_3D('',#10213,#7891,#7892);
#6296=AXIS2_PLACEMENT_3D('',#10216,#7894,#7895);
#6297=AXIS2_PLACEMENT_3D('',#10240,#7896,#7897);
#6298=AXIS2_PLACEMENT_3D('',#10241,#7898,#7899);
#6299=AXIS2_PLACEMENT_3D('',#10242,#7900,#7901);
#6300=AXIS2_PLACEMENT_3D('',#10243,#7902,#7903);
#6301=AXIS2_PLACEMENT_3D('',#10244,#7904,#7905);
#6302=AXIS2_PLACEMENT_3D('',#10245,#7906,#7907);
#6303=AXIS2_PLACEMENT_3D('',#10246,#7908,#7909);
#7800=DIRECTION('axis',(0.,0.,1.));
#7801=DIRECTION('refdir',(1.,0.,0.));
#7802=DIRECTION('center_axis',(0.,0.,1.));
#7803=DIRECTION('ref_axis',(1.,0.,0.));
#7804=DIRECTION('center_axis',(0.,-1.,0.));
#7805=DIRECTION('ref_axis',(0.,0.,-1.));
#7806=DIRECTION('center_axis',(0.,-1.,0.));
#7807=DIRECTION('ref_axis',(0.,0.,-1.));
#7808=DIRECTION('center_axis',(0.,1.,0.));
#7809=DIRECTION('ref_axis',(1.,0.,0.));
#7810=DIRECTION('center_axis',(0.,1.,0.));
#7811=DIRECTION('ref_axis',(1.,0.,0.));
#7812=DIRECTION('center_axis',(0.,1.,0.));
#7813=DIRECTION('ref_axis',(1.,0.,0.));
#7814=DIRECTION('center_axis',(0.,1.,0.));
#7815=DIRECTION('ref_axis',(1.,0.,0.));
#7816=DIRECTION('',(0.,-1.,0.));
#7817=DIRECTION('center_axis',(0.,-1.,0.));
#7818=DIRECTION('ref_axis',(1.,0.,0.));
#7819=DIRECTION('center_axis',(0.,1.,0.));
#7820=DIRECTION('ref_axis',(1.,0.,0.));
#7821=DIRECTION('center_axis',(0.,1.,0.));
#7822=DIRECTION('ref_axis',(1.,0.,0.));
#7823=DIRECTION('center_axis',(0.,1.,0.));
#7824=DIRECTION('ref_axis',(1.,0.,0.));
#7825=DIRECTION('center_axis',(0.,1.,0.));
#7826=DIRECTION('ref_axis',(1.,0.,0.));
#7827=DIRECTION('center_axis',(0.,1.,0.));
#7828=DIRECTION('ref_axis',(1.,0.,0.));
#7829=DIRECTION('center_axis',(0.,1.,0.));
#7830=DIRECTION('ref_axis',(1.,0.,0.));
#7831=DIRECTION('center_axis',(0.,-1.,0.));
#7832=DIRECTION('ref_axis',(1.,0.,0.));
#7833=DIRECTION('center_axis',(0.,-1.,0.));
#7834=DIRECTION('ref_axis',(0.,0.,-1.));
#7835=DIRECTION('center_axis',(6.12323399573677E-17,0.,1.));
#7836=DIRECTION('ref_axis',(1.,0.,0.));
#7837=DIRECTION('center_axis',(0.,-1.,0.));
#7838=DIRECTION('ref_axis',(0.,0.,-1.));
#7839=DIRECTION('center_axis',(0.,1.,0.));
#7840=DIRECTION('ref_axis',(1.,0.,0.));
#7841=DIRECTION('center_axis',(0.,-1.,0.));
#7842=DIRECTION('ref_axis',(1.,0.,0.));
#7843=DIRECTION('center_axis',(0.,-1.,0.));
#7844=DIRECTION('ref_axis',(0.,0.,-1.));
#7845=DIRECTION('center_axis',(0.,0.,1.));
#7846=DIRECTION('ref_axis',(1.,0.,0.));
#7847=DIRECTION('center_axis',(0.,-1.,0.));
#7848=DIRECTION('ref_axis',(0.,0.,-1.));
#7849=DIRECTION('center_axis',(0.,1.,0.));
#7850=DIRECTION('ref_axis',(1.,0.,0.));
#7851=DIRECTION('center_axis',(0.,-1.,0.));
#7852=DIRECTION('ref_axis',(1.,0.,0.));
#7853=DIRECTION('center_axis',(0.,-1.,0.));
#7854=DIRECTION('ref_axis',(0.,0.,-1.));
#7855=DIRECTION('center_axis',(0.,0.,1.));
#7856=DIRECTION('ref_axis',(1.,0.,0.));
#7857=DIRECTION('center_axis',(0.,-1.,0.));
#7858=DIRECTION('ref_axis',(0.,0.,-1.));
#7859=DIRECTION('center_axis',(0.,1.,0.));
#7860=DIRECTION('ref_axis',(1.,0.,0.));
#7861=DIRECTION('center_axis',(0.,-1.,0.));
#7862=DIRECTION('ref_axis',(1.,0.,0.));
#7863=DIRECTION('center_axis',(0.,-1.,0.));
#7864=DIRECTION('ref_axis',(0.,0.,-1.));
#7865=DIRECTION('center_axis',(0.,0.,1.));
#7866=DIRECTION('ref_axis',(1.,0.,0.));
#7867=DIRECTION('center_axis',(0.,-1.,0.));
#7868=DIRECTION('ref_axis',(0.,0.,-1.));
#7869=DIRECTION('center_axis',(0.,1.,0.));
#7870=DIRECTION('ref_axis',(1.,0.,0.));
#7871=DIRECTION('center_axis',(0.,-1.,0.));
#7872=DIRECTION('ref_axis',(1.,0.,0.));
#7873=DIRECTION('center_axis',(0.,-1.,0.));
#7874=DIRECTION('ref_axis',(0.,0.,-1.));
#7875=DIRECTION('center_axis',(6.12323399573676E-17,0.,1.));
#7876=DIRECTION('ref_axis',(1.,0.,0.));
#7877=DIRECTION('center_axis',(0.,-1.,0.));
#7878=DIRECTION('ref_axis',(0.,0.,-1.));
#7879=DIRECTION('center_axis',(0.,1.,0.));
#7880=DIRECTION('ref_axis',(1.,0.,0.));
#7881=DIRECTION('center_axis',(0.,-1.,0.));
#7882=DIRECTION('ref_axis',(1.,0.,0.));
#7883=DIRECTION('center_axis',(0.,-1.,0.));
#7884=DIRECTION('ref_axis',(0.,0.,-1.));
#7885=DIRECTION('center_axis',(0.,0.,1.));
#7886=DIRECTION('ref_axis',(1.,0.,0.));
#7887=DIRECTION('center_axis',(0.,-1.,0.));
#7888=DIRECTION('ref_axis',(0.,0.,-1.));
#7889=DIRECTION('center_axis',(0.,1.,0.));
#7890=DIRECTION('ref_axis',(1.,0.,0.));
#7891=DIRECTION('center_axis',(0.,1.,0.));
#7892=DIRECTION('ref_axis',(1.,0.,0.));
#7893=DIRECTION('',(0.,1.,0.));
#7894=DIRECTION('center_axis',(0.,-1.,0.));
#7895=DIRECTION('ref_axis',(1.,0.,0.));
#7896=DIRECTION('center_axis',(0.,-1.,0.));
#7897=DIRECTION('ref_axis',(1.,0.,0.));
#7898=DIRECTION('center_axis',(0.,1.,0.));
#7899=DIRECTION('ref_axis',(1.,0.,0.));
#7900=DIRECTION('center_axis',(0.,-1.,0.));
#7901=DIRECTION('ref_axis',(0.,0.,-1.));
#7902=DIRECTION('center_axis',(0.,0.,1.));
#7903=DIRECTION('ref_axis',(1.,0.,0.));
#7904=DIRECTION('center_axis',(0.,-1.,0.));
#7905=DIRECTION('ref_axis',(0.,0.,-1.));
#7906=DIRECTION('center_axis',(0.,-1.,0.));
#7907=DIRECTION('ref_axis',(-1.,0.,0.));
#7908=DIRECTION('center_axis',(0.,1.,0.));
#7909=DIRECTION('ref_axis',(1.,0.,0.));
#9799=CARTESIAN_POINT('',(0.,0.,0.));
#9800=CARTESIAN_POINT('Origin',(0.707106781186547,0.,0.707106781186548));
#9801=CARTESIAN_POINT('',(0.504455939115715,-0.04763,0.841298510752802));
#9802=CARTESIAN_POINT('',(0.841298510752802,-0.04763,0.504455939115715));
#9803=CARTESIAN_POINT('Ctrl Pts',(0.504455939115715,-0.04763,0.841298510752802));
#9804=CARTESIAN_POINT('Ctrl Pts',(0.508899795931835,-0.0740444353928835,
0.838633903678357));
#9805=CARTESIAN_POINT('Ctrl Pts',(0.517157748491652,-0.0999305678883309,
0.833661031856294));
#9806=CARTESIAN_POINT('Ctrl Pts',(0.537715343527944,-0.142345102874864,
0.820511285096538));
#9807=CARTESIAN_POINT('Ctrl Pts',(0.548874290046456,-0.159766064500479,
0.813159949759));
#9808=CARTESIAN_POINT('Ctrl Pts',(0.573915184558107,-0.190326085855194,
0.795684265985089));
#9809=CARTESIAN_POINT('Ctrl Pts',(0.587792702767295,-0.203463743702801,
0.78555112003688));
#9810=CARTESIAN_POINT('Ctrl Pts',(0.615966552324775,-0.224161999508995,
0.763642258217233));
#9811=CARTESIAN_POINT('Ctrl Pts',(0.631684198665438,-0.232861760990032,
0.750785745543687));
#9812=CARTESIAN_POINT('Ctrl Pts',(0.663382628119203,-0.244251601209411,
0.722929908501543));
#9813=CARTESIAN_POINT('Ctrl Pts',(0.679352081686668,-0.246942143572133,
0.707917883896095));
#9814=CARTESIAN_POINT('Ctrl Pts',(0.707917883896095,-0.246942143572133,
0.679352081686668));
#9815=CARTESIAN_POINT('Ctrl Pts',(0.722929908501543,-0.244251601209411,
0.663382628119203));
#9816=CARTESIAN_POINT('Ctrl Pts',(0.750785745543687,-0.232861760990032,
0.631684198665439));
#9817=CARTESIAN_POINT('Ctrl Pts',(0.763642258217232,-0.224161999508995,
0.615966552324775));
#9818=CARTESIAN_POINT('Ctrl Pts',(0.78555112003688,-0.203463743702801,0.587792702767295));
#9819=CARTESIAN_POINT('Ctrl Pts',(0.795684265985088,-0.190326085855194,
0.573915184558108));
#9820=CARTESIAN_POINT('Ctrl Pts',(0.813159949759,-0.15976606450048,0.548874290046456));
#9821=CARTESIAN_POINT('Ctrl Pts',(0.820511285096538,-0.142345102874864,
0.537715343527944));
#9822=CARTESIAN_POINT('Ctrl Pts',(0.833661031856294,-0.099930567888331,
0.517157748491653));
#9823=CARTESIAN_POINT('Ctrl Pts',(0.838633903678357,-0.0740444353928835,
0.508899795931835));
#9824=CARTESIAN_POINT('Ctrl Pts',(0.841298510752801,-0.0476299999999999,
0.504455939115715));
#9825=CARTESIAN_POINT('',(0.528110872004958,-0.04763,0.871530771444223));
#9826=CARTESIAN_POINT('Origin',(0.707106781186547,-0.04763,0.707106781186548));
#9827=CARTESIAN_POINT('',(0.871530771444223,-0.04763,0.528110872004959));
#9828=CARTESIAN_POINT('Ctrl Pts',(0.871530771444223,-0.0476300000000001,
0.528110872004958));
#9829=CARTESIAN_POINT('Ctrl Pts',(0.87014664509073,-0.0609922781173483,
0.530395067942936));
#9830=CARTESIAN_POINT('Ctrl Pts',(0.868149331745851,-0.0742967091364493,
0.533674141594226));
#9831=CARTESIAN_POINT('Ctrl Pts',(0.85981294420286,-0.115492077056649,0.54708917182331));
#9832=CARTESIAN_POINT('Ctrl Pts',(0.850993704737257,-0.141695629206859,
0.560922177770136));
#9833=CARTESIAN_POINT('Ctrl Pts',(0.830754510485543,-0.181890537957859,
0.590422647829571));
#9834=CARTESIAN_POINT('Ctrl Pts',(0.816896541396381,-0.201072148666545,
0.609616703125488));
#9835=CARTESIAN_POINT('Ctrl Pts',(0.792310597819928,-0.223955109275652,
0.641117951819998));
#9836=CARTESIAN_POINT('Ctrl Pts',(0.779109323683612,-0.232742381310829,
0.657208095763053));
#9837=CARTESIAN_POINT('Ctrl Pts',(0.750552691816206,-0.244234834628584,
0.68964083160521));
#9838=CARTESIAN_POINT('Ctrl Pts',(0.735185187071673,-0.246942143572133,
0.705971972091755));
#9839=CARTESIAN_POINT('Ctrl Pts',(0.705971972091754,-0.246942143572133,
0.735185187071673));
#9840=CARTESIAN_POINT('Ctrl Pts',(0.689640831605209,-0.244234834628584,
0.750552691816206));
#9841=CARTESIAN_POINT('Ctrl Pts',(0.657208095763052,-0.232742381310829,
0.779109323683612));
#9842=CARTESIAN_POINT('Ctrl Pts',(0.641117951819998,-0.223955109275652,
0.792310597819928));
#9843=CARTESIAN_POINT('Ctrl Pts',(0.609616703125487,-0.201072148666545,
0.816896541396382));
#9844=CARTESIAN_POINT('Ctrl Pts',(0.590422647829571,-0.181890537957858,
0.830754510485544));
#9845=CARTESIAN_POINT('Ctrl Pts',(0.560922177770135,-0.141695629206858,
0.850993704737257));
#9846=CARTESIAN_POINT('Ctrl Pts',(0.547089171823309,-0.115492077056649,
0.859812944202861));
#9847=CARTESIAN_POINT('Ctrl Pts',(0.533674141594226,-0.0742967091364491,
0.868149331745852));
#9848=CARTESIAN_POINT('Ctrl Pts',(0.530395067942936,-0.0609922781173483,
0.870146645090731));
#9849=CARTESIAN_POINT('Ctrl Pts',(0.528110872004958,-0.0476300000000001,
0.871530771444223));
#9850=CARTESIAN_POINT('Origin',(0.707106781186547,-0.04763,0.707106781186548));
#9851=CARTESIAN_POINT('Origin',(0.,-0.166705,0.));
#9852=CARTESIAN_POINT('',(0.242834539687906,-0.04763,0.989696097314));
#9853=CARTESIAN_POINT('Origin',(0.,-0.04763,0.));
#9854=CARTESIAN_POINT('',(-0.242834539687907,-0.04763,0.989696097314));
#9855=CARTESIAN_POINT('Ctrl Pts',(0.242834539687906,-0.04763,0.989696097314));
#9856=CARTESIAN_POINT('Ctrl Pts',(0.24024064412003,-0.0609922781173483,
0.990332542620729));
#9857=CARTESIAN_POINT('Ctrl Pts',(0.236509675094874,-0.0742967091364492,
0.991238884025248));
#9858=CARTESIAN_POINT('Ctrl Pts',(0.221129100087819,-0.115492077056649,
0.994830026707808));
#9859=CARTESIAN_POINT('Ctrl Pts',(0.205111543747588,-0.141695629206859,
0.998375294985966));
#9860=CARTESIAN_POINT('Ctrl Pts',(0.169940289819232,-0.181890537957859,
1.00492400591205));
#9861=CARTESIAN_POINT('Ctrl Pts',(0.1465689792446,-0.201072148666545,1.00869718865384));
#9862=CARTESIAN_POINT('Ctrl Pts',(0.106909345252087,-0.223955109275652,
1.01358704779679));
#9863=CARTESIAN_POINT('Ctrl Pts',(0.0861971848975941,-0.232742381310829,
1.0156297872271));
#9864=CARTESIAN_POINT('Ctrl Pts',(0.0430711894098822,-0.244234834628584,
1.01837060663223));
#9865=CARTESIAN_POINT('Ctrl Pts',(0.0206568624125605,-0.246942143572133,
1.019052));
#9866=CARTESIAN_POINT('Ctrl Pts',(-0.0206568624125608,-0.246942143572133,
1.019052));
#9867=CARTESIAN_POINT('Ctrl Pts',(-0.0430711894098825,-0.244234834628584,
1.01837060663223));
#9868=CARTESIAN_POINT('Ctrl Pts',(-0.0861971848975943,-0.232742381310829,
1.0156297872271));
#9869=CARTESIAN_POINT('Ctrl Pts',(-0.106909345252088,-0.223955109275652,
1.01358704779679));
#9870=CARTESIAN_POINT('Ctrl Pts',(-0.1465689792446,-0.201072148666545,1.00869718865384));
#9871=CARTESIAN_POINT('Ctrl Pts',(-0.169940289819232,-0.181890537957859,
1.00492400591205));
#9872=CARTESIAN_POINT('Ctrl Pts',(-0.205111543747588,-0.141695629206859,
0.998375294985966));
#9873=CARTESIAN_POINT('Ctrl Pts',(-0.221129100087819,-0.115492077056649,
0.994830026707808));
#9874=CARTESIAN_POINT('Ctrl Pts',(-0.236509675094875,-0.0742967091364493,
0.991238884025248));
#9875=CARTESIAN_POINT('Ctrl Pts',(-0.24024064412003,-0.0609922781173483,
0.990332542620729));
#9876=CARTESIAN_POINT('Ctrl Pts',(-0.242834539687907,-0.04763,0.989696097314));
#9877=CARTESIAN_POINT('',(-0.528110872004959,-0.04763,0.871530771444223));
#9878=CARTESIAN_POINT('Origin',(0.,-0.04763,0.));
#9879=CARTESIAN_POINT('',(-0.871530771444223,-0.04763,0.528110872004958));
#9880=CARTESIAN_POINT('Ctrl Pts',(-0.528110872004958,-0.0476300000000001,
0.871530771444223));
#9881=CARTESIAN_POINT('Ctrl Pts',(-0.530395067942936,-0.0609922781173484,
0.87014664509073));
#9882=CARTESIAN_POINT('Ctrl Pts',(-0.533674141594226,-0.0742967091364493,
0.868149331745851));
#9883=CARTESIAN_POINT('Ctrl Pts',(-0.54708917182331,-0.115492077056649,
0.85981294420286));
#9884=CARTESIAN_POINT('Ctrl Pts',(-0.560922177770136,-0.141695629206859,
0.850993704737257));
#9885=CARTESIAN_POINT('Ctrl Pts',(-0.590422647829571,-0.181890537957859,
0.830754510485543));
#9886=CARTESIAN_POINT('Ctrl Pts',(-0.609616703125488,-0.201072148666545,
0.816896541396381));
#9887=CARTESIAN_POINT('Ctrl Pts',(-0.641117951819998,-0.223955109275652,
0.792310597819928));
#9888=CARTESIAN_POINT('Ctrl Pts',(-0.657208095763053,-0.232742381310829,
0.779109323683611));
#9889=CARTESIAN_POINT('Ctrl Pts',(-0.68964083160521,-0.244234834628584,
0.750552691816205));
#9890=CARTESIAN_POINT('Ctrl Pts',(-0.705971972091755,-0.246942143572133,
0.735185187071673));
#9891=CARTESIAN_POINT('Ctrl Pts',(-0.735185187071673,-0.246942143572133,
0.705971972091754));
#9892=CARTESIAN_POINT('Ctrl Pts',(-0.750552691816206,-0.244234834628584,
0.689640831605209));
#9893=CARTESIAN_POINT('Ctrl Pts',(-0.779109323683612,-0.232742381310829,
0.657208095763052));
#9894=CARTESIAN_POINT('Ctrl Pts',(-0.792310597819928,-0.223955109275652,
0.641117951819998));
#9895=CARTESIAN_POINT('Ctrl Pts',(-0.816896541396382,-0.201072148666545,
0.609616703125487));
#9896=CARTESIAN_POINT('Ctrl Pts',(-0.830754510485544,-0.181890537957858,
0.590422647829571));
#9897=CARTESIAN_POINT('Ctrl Pts',(-0.850993704737257,-0.141695629206858,
0.560922177770135));
#9898=CARTESIAN_POINT('Ctrl Pts',(-0.859812944202861,-0.115492077056649,
0.547089171823309));
#9899=CARTESIAN_POINT('Ctrl Pts',(-0.868149331745852,-0.0742967091364491,
0.533674141594226));
#9900=CARTESIAN_POINT('Ctrl Pts',(-0.870146645090731,-0.0609922781173483,
0.530395067942936));
#9901=CARTESIAN_POINT('Ctrl Pts',(-0.871530771444223,-0.04763,0.528110872004958));
#9902=CARTESIAN_POINT('',(-0.989696097314,-0.04763,0.242834539687906));
#9903=CARTESIAN_POINT('Origin',(0.,-0.04763,0.));
#9904=CARTESIAN_POINT('',(-1.019052,-0.246942143572133,1.248489836334E-16));
#9905=CARTESIAN_POINT('Ctrl Pts',(-0.989696097314,-0.04763,0.242834539687906));
#9906=CARTESIAN_POINT('Ctrl Pts',(-0.990332542620729,-0.0609922781173483,
0.24024064412003));
#9907=CARTESIAN_POINT('Ctrl Pts',(-0.991238884025248,-0.0742967091364492,
0.236509675094874));
#9908=CARTESIAN_POINT('Ctrl Pts',(-0.994830026707808,-0.115492077056649,
0.221129100087819));
#9909=CARTESIAN_POINT('Ctrl Pts',(-0.998375294985966,-0.141695629206859,
0.205111543747588));
#9910=CARTESIAN_POINT('Ctrl Pts',(-1.00492400591205,-0.181890537957859,
0.169940289819232));
#9911=CARTESIAN_POINT('Ctrl Pts',(-1.00869718865384,-0.201072148666545,
0.1465689792446));
#9912=CARTESIAN_POINT('Ctrl Pts',(-1.01358704779679,-0.223955109275652,
0.106909345252088));
#9913=CARTESIAN_POINT('Ctrl Pts',(-1.0156297872271,-0.232742381310829,0.0861971848975944));
#9914=CARTESIAN_POINT('Ctrl Pts',(-1.01837060663223,-0.244234834628584,
0.0430711894098825));
#9915=CARTESIAN_POINT('Ctrl Pts',(-1.019052,-0.246942143572133,0.0206568624125608));
#9916=CARTESIAN_POINT('Ctrl Pts',(-1.019052,-0.246942143572133,1.2490009027033E-16));
#9917=CARTESIAN_POINT('',(-1.019052,-0.28578,1.24797876996471E-16));
#9918=CARTESIAN_POINT('',(-1.019052,-0.166705,1.24797876996471E-16));
#9919=CARTESIAN_POINT('Origin',(0.,-0.28578,0.));
#9920=CARTESIAN_POINT('',(-0.989696097314,-0.04763,-0.242834539687906));
#9921=CARTESIAN_POINT('Ctrl Pts',(-1.019052,-0.246942143572133,1.2490009027033E-16));
#9922=CARTESIAN_POINT('Ctrl Pts',(-1.019052,-0.246942143572133,-0.0206568624125605));
#9923=CARTESIAN_POINT('Ctrl Pts',(-1.01837060663223,-0.244234834628584,
-0.0430711894098822));
#9924=CARTESIAN_POINT('Ctrl Pts',(-1.0156297872271,-0.232742381310829,-0.0861971848975941));
#9925=CARTESIAN_POINT('Ctrl Pts',(-1.01358704779679,-0.223955109275652,
-0.106909345252087));
#9926=CARTESIAN_POINT('Ctrl Pts',(-1.00869718865384,-0.201072148666546,
-0.1465689792446));
#9927=CARTESIAN_POINT('Ctrl Pts',(-1.00492400591205,-0.181890537957859,
-0.169940289819232));
#9928=CARTESIAN_POINT('Ctrl Pts',(-0.998375294985966,-0.141695629206859,
-0.205111543747588));
#9929=CARTESIAN_POINT('Ctrl Pts',(-0.994830026707808,-0.11549207705665,
-0.221129100087819));
#9930=CARTESIAN_POINT('Ctrl Pts',(-0.991238884025248,-0.0742967091364495,
-0.236509675094874));
#9931=CARTESIAN_POINT('Ctrl Pts',(-0.990332542620729,-0.0609922781173484,
-0.24024064412003));
#9932=CARTESIAN_POINT('Ctrl Pts',(-0.989696097314,-0.0476300000000001,-0.242834539687907));
#9933=CARTESIAN_POINT('',(-0.871530771444223,-0.04763,-0.528110872004958));
#9934=CARTESIAN_POINT('Origin',(0.,-0.04763,0.));
#9935=CARTESIAN_POINT('',(-0.528110872004958,-0.04763,-0.871530771444223));
#9936=CARTESIAN_POINT('Ctrl Pts',(-0.871530771444223,-0.0476300000000001,
-0.528110872004958));
#9937=CARTESIAN_POINT('Ctrl Pts',(-0.87014664509073,-0.0609922781173484,
-0.530395067942936));
#9938=CARTESIAN_POINT('Ctrl Pts',(-0.868149331745851,-0.0742967091364494,
-0.533674141594226));
#9939=CARTESIAN_POINT('Ctrl Pts',(-0.85981294420286,-0.115492077056649,
-0.54708917182331));
#9940=CARTESIAN_POINT('Ctrl Pts',(-0.850993704737257,-0.141695629206859,
-0.560922177770136));
#9941=CARTESIAN_POINT('Ctrl Pts',(-0.830754510485543,-0.181890537957859,
-0.590422647829571));
#9942=CARTESIAN_POINT('Ctrl Pts',(-0.816896541396381,-0.201072148666546,
-0.609616703125488));
#9943=CARTESIAN_POINT('Ctrl Pts',(-0.792310597819928,-0.223955109275652,
-0.641117951819999));
#9944=CARTESIAN_POINT('Ctrl Pts',(-0.779109323683611,-0.232742381310829,
-0.657208095763053));
#9945=CARTESIAN_POINT('Ctrl Pts',(-0.750552691816205,-0.244234834628584,
-0.68964083160521));
#9946=CARTESIAN_POINT('Ctrl Pts',(-0.735185187071673,-0.246942143572133,
-0.705971972091755));
#9947=CARTESIAN_POINT('Ctrl Pts',(-0.705971972091754,-0.246942143572133,
-0.735185187071673));
#9948=CARTESIAN_POINT('Ctrl Pts',(-0.68964083160521,-0.244234834628584,
-0.750552691816206));
#9949=CARTESIAN_POINT('Ctrl Pts',(-0.657208095763052,-0.232742381310829,
-0.779109323683612));
#9950=CARTESIAN_POINT('Ctrl Pts',(-0.641117951819998,-0.223955109275652,
-0.792310597819928));
#9951=CARTESIAN_POINT('Ctrl Pts',(-0.609616703125488,-0.201072148666545,
-0.816896541396381));
#9952=CARTESIAN_POINT('Ctrl Pts',(-0.590422647829571,-0.181890537957859,
-0.830754510485543));
#9953=CARTESIAN_POINT('Ctrl Pts',(-0.560922177770136,-0.141695629206859,
-0.850993704737257));
#9954=CARTESIAN_POINT('Ctrl Pts',(-0.54708917182331,-0.115492077056649,
-0.85981294420286));
#9955=CARTESIAN_POINT('Ctrl Pts',(-0.533674141594226,-0.0742967091364494,
-0.868149331745852));
#9956=CARTESIAN_POINT('Ctrl Pts',(-0.530395067942936,-0.0609922781173484,
-0.870146645090731));
#9957=CARTESIAN_POINT('Ctrl Pts',(-0.528110872004958,-0.0476300000000001,
-0.871530771444223));
#9958=CARTESIAN_POINT('',(-0.242834539687906,-0.04763,-0.989696097314));
#9959=CARTESIAN_POINT('Origin',(0.,-0.04763,0.));
#9960=CARTESIAN_POINT('',(0.242834539687906,-0.04763,-0.989696097314));
#9961=CARTESIAN_POINT('Ctrl Pts',(-0.242834539687907,-0.04763,-0.989696097314));
#9962=CARTESIAN_POINT('Ctrl Pts',(-0.24024064412003,-0.0609922781173483,
-0.990332542620729));
#9963=CARTESIAN_POINT('Ctrl Pts',(-0.236509675094874,-0.0742967091364493,
-0.991238884025248));
#9964=CARTESIAN_POINT('Ctrl Pts',(-0.221129100087819,-0.115492077056649,
-0.994830026707808));
#9965=CARTESIAN_POINT('Ctrl Pts',(-0.205111543747588,-0.141695629206859,
-0.998375294985966));
#9966=CARTESIAN_POINT('Ctrl Pts',(-0.169940289819232,-0.181890537957859,
-1.00492400591205));
#9967=CARTESIAN_POINT('Ctrl Pts',(-0.1465689792446,-0.201072148666545,-1.00869718865384));
#9968=CARTESIAN_POINT('Ctrl Pts',(-0.106909345252087,-0.223955109275652,
-1.01358704779679));
#9969=CARTESIAN_POINT('Ctrl Pts',(-0.0861971848975942,-0.232742381310829,
-1.0156297872271));
#9970=CARTESIAN_POINT('Ctrl Pts',(-0.0430711894098823,-0.244234834628584,
-1.01837060663223));
#9971=CARTESIAN_POINT('Ctrl Pts',(-0.0206568624125606,-0.246942143572133,
-1.019052));
#9972=CARTESIAN_POINT('Ctrl Pts',(0.0206568624125607,-0.246942143572133,
-1.019052));
#9973=CARTESIAN_POINT('Ctrl Pts',(0.0430711894098824,-0.244234834628584,
-1.01837060663223));
#9974=CARTESIAN_POINT('Ctrl Pts',(0.0861971848975943,-0.232742381310829,
-1.0156297872271));
#9975=CARTESIAN_POINT('Ctrl Pts',(0.106909345252088,-0.223955109275652,
-1.01358704779679));
#9976=CARTESIAN_POINT('Ctrl Pts',(0.1465689792446,-0.201072148666545,-1.00869718865384));
#9977=CARTESIAN_POINT('Ctrl Pts',(0.169940289819232,-0.181890537957859,
-1.00492400591205));
#9978=CARTESIAN_POINT('Ctrl Pts',(0.205111543747588,-0.141695629206859,
-0.998375294985966));
#9979=CARTESIAN_POINT('Ctrl Pts',(0.221129100087819,-0.115492077056649,
-0.994830026707808));
#9980=CARTESIAN_POINT('Ctrl Pts',(0.236509675094874,-0.0742967091364493,
-0.991238884025248));
#9981=CARTESIAN_POINT('Ctrl Pts',(0.24024064412003,-0.0609922781173484,
-0.990332542620729));
#9982=CARTESIAN_POINT('Ctrl Pts',(0.242834539687907,-0.04763,-0.989696097314));
#9983=CARTESIAN_POINT('',(0.528110872004958,-0.04763,-0.871530771444223));
#9984=CARTESIAN_POINT('Origin',(0.,-0.04763,0.));
#9985=CARTESIAN_POINT('',(0.871530771444223,-0.04763,-0.528110872004958));
#9986=CARTESIAN_POINT('Ctrl Pts',(0.528110872004958,-0.0476300000000001,
-0.871530771444223));
#9987=CARTESIAN_POINT('Ctrl Pts',(0.530395067942936,-0.0609922781173484,
-0.870146645090731));
#9988=CARTESIAN_POINT('Ctrl Pts',(0.533674141594226,-0.0742967091364493,
-0.868149331745851));
#9989=CARTESIAN_POINT('Ctrl Pts',(0.54708917182331,-0.115492077056649,-0.85981294420286));
#9990=CARTESIAN_POINT('Ctrl Pts',(0.560922177770136,-0.141695629206859,
-0.850993704737257));
#9991=CARTESIAN_POINT('Ctrl Pts',(0.590422647829571,-0.181890537957859,
-0.830754510485543));
#9992=CARTESIAN_POINT('Ctrl Pts',(0.609616703125488,-0.201072148666545,
-0.816896541396381));
#9993=CARTESIAN_POINT('Ctrl Pts',(0.641117951819998,-0.223955109275652,
-0.792310597819928));
#9994=CARTESIAN_POINT('Ctrl Pts',(0.657208095763053,-0.232742381310829,
-0.779109323683612));
#9995=CARTESIAN_POINT('Ctrl Pts',(0.68964083160521,-0.244234834628584,-0.750552691816206));
#9996=CARTESIAN_POINT('Ctrl Pts',(0.705971972091755,-0.246942143572133,
-0.735185187071673));
#9997=CARTESIAN_POINT('Ctrl Pts',(0.735185187071673,-0.246942143572133,
-0.705971972091754));
#9998=CARTESIAN_POINT('Ctrl Pts',(0.750552691816206,-0.244234834628584,
-0.68964083160521));
#9999=CARTESIAN_POINT('Ctrl Pts',(0.779109323683612,-0.232742381310829,
-0.657208095763053));
#10000=CARTESIAN_POINT('Ctrl Pts',(0.792310597819928,-0.223955109275652,
-0.641117951819998));
#10001=CARTESIAN_POINT('Ctrl Pts',(0.816896541396381,-0.201072148666545,
-0.609616703125488));
#10002=CARTESIAN_POINT('Ctrl Pts',(0.830754510485543,-0.181890537957859,
-0.590422647829571));
#10003=CARTESIAN_POINT('Ctrl Pts',(0.850993704737257,-0.141695629206859,
-0.560922177770136));
#10004=CARTESIAN_POINT('Ctrl Pts',(0.85981294420286,-0.115492077056649,
-0.54708917182331));
#10005=CARTESIAN_POINT('Ctrl Pts',(0.868149331745851,-0.0742967091364493,
-0.533674141594226));
#10006=CARTESIAN_POINT('Ctrl Pts',(0.870146645090731,-0.0609922781173484,
-0.530395067942936));
#10007=CARTESIAN_POINT('Ctrl Pts',(0.871530771444223,-0.0476300000000001,
-0.528110872004958));
#10008=CARTESIAN_POINT('',(0.989696097314,-0.04763,-0.242834539687906));
#10009=CARTESIAN_POINT('Origin',(0.,-0.04763,0.));
#10010=CARTESIAN_POINT('',(0.989696097314,-0.04763,0.242834539687906));
#10011=CARTESIAN_POINT('Ctrl Pts',(0.989696097314,-0.04763,-0.242834539687907));
#10012=CARTESIAN_POINT('Ctrl Pts',(0.990332542620729,-0.0609922781173483,
-0.24024064412003));
#10013=CARTESIAN_POINT('Ctrl Pts',(0.991238884025248,-0.0742967091364493,
-0.236509675094874));
#10014=CARTESIAN_POINT('Ctrl Pts',(0.994830026707808,-0.115492077056649,
-0.221129100087819));
#10015=CARTESIAN_POINT('Ctrl Pts',(0.998375294985966,-0.141695629206859,
-0.205111543747588));
#10016=CARTESIAN_POINT('Ctrl Pts',(1.00492400591205,-0.181890537957859,
-0.169940289819232));
#10017=CARTESIAN_POINT('Ctrl Pts',(1.00869718865384,-0.201072148666545,
-0.1465689792446));
#10018=CARTESIAN_POINT('Ctrl Pts',(1.01358704779679,-0.223955109275652,
-0.106909345252087));
#10019=CARTESIAN_POINT('Ctrl Pts',(1.0156297872271,-0.232742381310829,-0.0861971848975942));
#10020=CARTESIAN_POINT('Ctrl Pts',(1.01837060663223,-0.244234834628584,
-0.0430711894098823));
#10021=CARTESIAN_POINT('Ctrl Pts',(1.019052,-0.246942143572133,-0.0206568624125607));
#10022=CARTESIAN_POINT('Ctrl Pts',(1.019052,-0.246942143572133,0.0206568624125607));
#10023=CARTESIAN_POINT('Ctrl Pts',(1.01837060663223,-0.244234834628584,
0.0430711894098823));
#10024=CARTESIAN_POINT('Ctrl Pts',(1.0156297872271,-0.232742381310829,0.0861971848975942));
#10025=CARTESIAN_POINT('Ctrl Pts',(1.01358704779679,-0.223955109275652,
0.106909345252087));
#10026=CARTESIAN_POINT('Ctrl Pts',(1.00869718865384,-0.201072148666545,
0.1465689792446));
#10027=CARTESIAN_POINT('Ctrl Pts',(1.00492400591205,-0.181890537957859,
0.169940289819232));
#10028=CARTESIAN_POINT('Ctrl Pts',(0.998375294985966,-0.141695629206859,
0.205111543747588));
#10029=CARTESIAN_POINT('Ctrl Pts',(0.994830026707808,-0.115492077056649,
0.221129100087819));
#10030=CARTESIAN_POINT('Ctrl Pts',(0.991238884025248,-0.0742967091364492,
0.236509675094874));
#10031=CARTESIAN_POINT('Ctrl Pts',(0.990332542620729,-0.0609922781173483,
0.24024064412003));
#10032=CARTESIAN_POINT('Ctrl Pts',(0.989696097314,-0.04763,0.242834539687907));
#10033=CARTESIAN_POINT('Origin',(0.,-0.04763,0.));
#10034=CARTESIAN_POINT('Origin',(0.,-0.04763,0.));
#10035=CARTESIAN_POINT('',(0.238183666596899,-0.04763,0.951592097314));
#10036=CARTESIAN_POINT('Origin',(0.,-0.04763,0.));
#10037=CARTESIAN_POINT('Origin',(-1.94289029309402E-16,-0.04763,1.));
#10038=CARTESIAN_POINT('Origin',(-1.94289029309402E-16,0.,1.));
#10039=CARTESIAN_POINT('',(-0.2381836665969,-0.04763,0.951592097314));
#10040=CARTESIAN_POINT('Ctrl Pts',(-0.238183666596899,-0.0476299999999999,
0.951592097314));
#10041=CARTESIAN_POINT('Ctrl Pts',(-0.233157223576062,-0.0740444353928835,
0.952850216871763));
#10042=CARTESIAN_POINT('Ctrl Pts',(-0.223801617934946,-0.0999305678883309,
0.955173119738174));
#10043=CARTESIAN_POINT('Ctrl Pts',(-0.199966927975188,-0.142345102874864,
0.960411259488514));
#10044=CARTESIAN_POINT('Ctrl Pts',(-0.1868781821531,-0.159766064500479,
0.963103647174702));
#10045=CARTESIAN_POINT('Ctrl Pts',(-0.15681442133453,-0.190326085855194,
0.968453058988463));
#10046=CARTESIAN_POINT('Ctrl Pts',(-0.139836317888043,-0.203463743702801,
0.971100730005489));
#10047=CARTESIAN_POINT('Ctrl Pts',(-0.104422493053067,-0.224161999508995,
0.975530745318961));
#10048=CARTESIAN_POINT('Ctrl Pts',(-0.0842175114474176,-0.232861760990032,
0.977553872336861));
#10049=CARTESIAN_POINT('Ctrl Pts',(-0.0421062857595701,-0.244251601209411,
0.980270995488453));
#10050=CARTESIAN_POINT('Ctrl Pts',(-0.0201990724523197,-0.246942143572133,
0.980948));
#10051=CARTESIAN_POINT('Ctrl Pts',(0.020199072452319,-0.246942143572133,
0.980948));
#10052=CARTESIAN_POINT('Ctrl Pts',(0.0421062857595694,-0.244251601209411,
0.980270995488454));
#10053=CARTESIAN_POINT('Ctrl Pts',(0.0842175114474169,-0.232861760990032,
0.977553872336861));
#10054=CARTESIAN_POINT('Ctrl Pts',(0.104422493053067,-0.224161999508995,
0.975530745318961));
#10055=CARTESIAN_POINT('Ctrl Pts',(0.139836317888042,-0.203463743702801,
0.971100730005489));
#10056=CARTESIAN_POINT('Ctrl Pts',(0.15681442133453,-0.190326085855194,
0.968453058988463));
#10057=CARTESIAN_POINT('Ctrl Pts',(0.1868781821531,-0.15976606450048,0.963103647174702));
#10058=CARTESIAN_POINT('Ctrl Pts',(0.199966927975188,-0.142345102874864,
0.960411259488514));
#10059=CARTESIAN_POINT('Ctrl Pts',(0.223801617934945,-0.0999305678883309,
0.955173119738174));
#10060=CARTESIAN_POINT('Ctrl Pts',(0.233157223576061,-0.0740444353928835,
0.952850216871763));
#10061=CARTESIAN_POINT('Ctrl Pts',(0.238183666596899,-0.0476299999999999,
0.951592097314));
#10062=CARTESIAN_POINT('Origin',(-1.94289029309402E-16,-0.04763,1.));
#10063=CARTESIAN_POINT('Origin',(0.,-0.04763,0.));
#10064=CARTESIAN_POINT('',(-0.504455939115715,-0.04763,0.841298510752802));
#10065=CARTESIAN_POINT('Origin',(0.,-0.04763,0.));
#10066=CARTESIAN_POINT('Origin',(-0.707106781186548,-0.04763,0.707106781186547));
#10067=CARTESIAN_POINT('Origin',(-0.707106781186548,0.,0.707106781186547));
#10068=CARTESIAN_POINT('',(-0.841298510752802,-0.04763,0.504455939115715));
#10069=CARTESIAN_POINT('Ctrl Pts',(-0.841298510752802,-0.04763,0.504455939115715));
#10070=CARTESIAN_POINT('Ctrl Pts',(-0.838633903678357,-0.0740444353928835,
0.508899795931835));
#10071=CARTESIAN_POINT('Ctrl Pts',(-0.833661031856294,-0.0999305678883309,
0.517157748491652));
#10072=CARTESIAN_POINT('Ctrl Pts',(-0.820511285096538,-0.142345102874864,
0.537715343527944));
#10073=CARTESIAN_POINT('Ctrl Pts',(-0.813159949759,-0.159766064500479,0.548874290046456));
#10074=CARTESIAN_POINT('Ctrl Pts',(-0.795684265985089,-0.190326085855194,
0.573915184558107));
#10075=CARTESIAN_POINT('Ctrl Pts',(-0.78555112003688,-0.203463743702801,
0.587792702767295));
#10076=CARTESIAN_POINT('Ctrl Pts',(-0.763642258217233,-0.224161999508995,
0.615966552324775));
#10077=CARTESIAN_POINT('Ctrl Pts',(-0.750785745543687,-0.232861760990032,
0.631684198665438));
#10078=CARTESIAN_POINT('Ctrl Pts',(-0.722929908501543,-0.244251601209411,
0.663382628119203));
#10079=CARTESIAN_POINT('Ctrl Pts',(-0.707917883896095,-0.246942143572133,
0.679352081686668));
#10080=CARTESIAN_POINT('Ctrl Pts',(-0.679352081686668,-0.246942143572133,
0.707917883896095));
#10081=CARTESIAN_POINT('Ctrl Pts',(-0.663382628119203,-0.244251601209411,
0.722929908501544));
#10082=CARTESIAN_POINT('Ctrl Pts',(-0.631684198665438,-0.232861760990031,
0.750785745543687));
#10083=CARTESIAN_POINT('Ctrl Pts',(-0.615966552324775,-0.224161999508995,
0.763642258217233));
#10084=CARTESIAN_POINT('Ctrl Pts',(-0.587792702767295,-0.203463743702801,
0.78555112003688));
#10085=CARTESIAN_POINT('Ctrl Pts',(-0.573915184558107,-0.190326085855194,
0.795684265985088));
#10086=CARTESIAN_POINT('Ctrl Pts',(-0.548874290046456,-0.159766064500479,
0.813159949759));
#10087=CARTESIAN_POINT('Ctrl Pts',(-0.537715343527944,-0.142345102874864,
0.820511285096538));
#10088=CARTESIAN_POINT('Ctrl Pts',(-0.517157748491652,-0.0999305678883309,
0.833661031856294));
#10089=CARTESIAN_POINT('Ctrl Pts',(-0.508899795931835,-0.0740444353928835,
0.838633903678357));
#10090=CARTESIAN_POINT('Ctrl Pts',(-0.504455939115716,-0.04763,0.841298510752801));
#10091=CARTESIAN_POINT('Origin',(-0.707106781186548,-0.04763,0.707106781186547));
#10092=CARTESIAN_POINT('Origin',(0.,-0.04763,0.));
#10093=CARTESIAN_POINT('',(-0.951592097314,-0.04763,0.238183666596899));
#10094=CARTESIAN_POINT('Origin',(0.,-0.04763,0.));
#10095=CARTESIAN_POINT('Origin',(-1.,-0.04763,-1.11022302462516E-16));
#10096=CARTESIAN_POINT('Origin',(-1.,0.,-1.11022302462516E-16));
#10097=CARTESIAN_POINT('',(-0.951592097314,-0.04763,-0.2381836665969));
#10098=CARTESIAN_POINT('',(-0.980948,-0.246942143572133,1.08514323328844E-18));
#10099=CARTESIAN_POINT('Ctrl Pts',(-0.951592097314,-0.04763,-0.238183666596899));
#10100=CARTESIAN_POINT('Ctrl Pts',(-0.952850216871763,-0.0740444353928835,
-0.233157223576062));
#10101=CARTESIAN_POINT('Ctrl Pts',(-0.955173119738174,-0.0999305678883309,
-0.223801617934946));
#10102=CARTESIAN_POINT('Ctrl Pts',(-0.960411259488514,-0.142345102874864,
-0.199966927975188));
#10103=CARTESIAN_POINT('Ctrl Pts',(-0.963103647174702,-0.159766064500479,
-0.1868781821531));
#10104=CARTESIAN_POINT('Ctrl Pts',(-0.968453058988463,-0.190326085855194,
-0.15681442133453));
#10105=CARTESIAN_POINT('Ctrl Pts',(-0.971100730005489,-0.203463743702801,
-0.139836317888043));
#10106=CARTESIAN_POINT('Ctrl Pts',(-0.975530745318961,-0.224161999508995,
-0.104422493053067));
#10107=CARTESIAN_POINT('Ctrl Pts',(-0.977553872336861,-0.232861760990032,
-0.0842175114474175));
#10108=CARTESIAN_POINT('Ctrl Pts',(-0.980270995488453,-0.244251601209411,
-0.0421062857595699));
#10109=CARTESIAN_POINT('Ctrl Pts',(-0.980948,-0.246942143572133,-0.0201990724523195));
#10110=CARTESIAN_POINT('Ctrl Pts',(-0.980948,-0.246942143572133,-1.17961196366423E-16));
#10111=CARTESIAN_POINT('Origin',(-1.,-0.04763,-1.11022302462516E-16));
#10112=CARTESIAN_POINT('Ctrl Pts',(-0.980948,-0.246942143572133,-1.17961196366423E-16));
#10113=CARTESIAN_POINT('Ctrl Pts',(-0.980948,-0.246942143572133,0.0201990724523192));
#10114=CARTESIAN_POINT('Ctrl Pts',(-0.980270995488453,-0.244251601209411,
0.0421062857595695));
#10115=CARTESIAN_POINT('Ctrl Pts',(-0.977553872336861,-0.232861760990032,
0.0842175114474169));
#10116=CARTESIAN_POINT('Ctrl Pts',(-0.975530745318961,-0.224161999508995,
0.104422493053066));
#10117=CARTESIAN_POINT('Ctrl Pts',(-0.971100730005489,-0.203463743702801,
0.139836317888042));
#10118=CARTESIAN_POINT('Ctrl Pts',(-0.968453058988463,-0.190326085855194,
0.15681442133453));
#10119=CARTESIAN_POINT('Ctrl Pts',(-0.963103647174702,-0.15976606450048,
0.1868781821531));
#10120=CARTESIAN_POINT('Ctrl Pts',(-0.960411259488514,-0.142345102874864,
0.199966927975188));
#10121=CARTESIAN_POINT('Ctrl Pts',(-0.955173119738174,-0.099930567888331,
0.223801617934945));
#10122=CARTESIAN_POINT('Ctrl Pts',(-0.952850216871763,-0.0740444353928835,
0.233157223576061));
#10123=CARTESIAN_POINT('Ctrl Pts',(-0.951592097314,-0.04763,0.238183666596899));
#10124=CARTESIAN_POINT('Origin',(0.,-0.04763,0.));
#10125=CARTESIAN_POINT('',(-0.841298510752802,-0.04763,-0.504455939115715));
#10126=CARTESIAN_POINT('Origin',(0.,-0.04763,0.));
#10127=CARTESIAN_POINT('Origin',(-0.707106781186547,-0.04763,-0.707106781186548));
#10128=CARTESIAN_POINT('Origin',(-0.707106781186547,0.,-0.707106781186548));
#10129=CARTESIAN_POINT('',(-0.504455939115715,-0.04763,-0.841298510752802));
#10130=CARTESIAN_POINT('Ctrl Pts',(-0.504455939115715,-0.04763,-0.841298510752802));
#10131=CARTESIAN_POINT('Ctrl Pts',(-0.508899795931835,-0.0740444353928835,
-0.838633903678357));
#10132=CARTESIAN_POINT('Ctrl Pts',(-0.517157748491652,-0.0999305678883309,
-0.833661031856294));
#10133=CARTESIAN_POINT('Ctrl Pts',(-0.537715343527944,-0.142345102874864,
-0.820511285096538));
#10134=CARTESIAN_POINT('Ctrl Pts',(-0.548874290046456,-0.159766064500479,
-0.813159949759));
#10135=CARTESIAN_POINT('Ctrl Pts',(-0.573915184558107,-0.190326085855194,
-0.795684265985089));
#10136=CARTESIAN_POINT('Ctrl Pts',(-0.587792702767295,-0.203463743702801,
-0.78555112003688));
#10137=CARTESIAN_POINT('Ctrl Pts',(-0.615966552324775,-0.224161999508995,
-0.763642258217233));
#10138=CARTESIAN_POINT('Ctrl Pts',(-0.631684198665438,-0.232861760990032,
-0.750785745543687));
#10139=CARTESIAN_POINT('Ctrl Pts',(-0.663382628119203,-0.244251601209411,
-0.722929908501543));
#10140=CARTESIAN_POINT('Ctrl Pts',(-0.679352081686668,-0.246942143572133,
-0.707917883896095));
#10141=CARTESIAN_POINT('Ctrl Pts',(-0.707917883896095,-0.246942143572133,
-0.679352081686668));
#10142=CARTESIAN_POINT('Ctrl Pts',(-0.722929908501543,-0.244251601209411,
-0.663382628119203));
#10143=CARTESIAN_POINT('Ctrl Pts',(-0.750785745543687,-0.232861760990032,
-0.631684198665439));
#10144=CARTESIAN_POINT('Ctrl Pts',(-0.763642258217232,-0.224161999508995,
-0.615966552324775));
#10145=CARTESIAN_POINT('Ctrl Pts',(-0.78555112003688,-0.203463743702801,
-0.587792702767295));
#10146=CARTESIAN_POINT('Ctrl Pts',(-0.795684265985088,-0.190326085855194,
-0.573915184558107));
#10147=CARTESIAN_POINT('Ctrl Pts',(-0.813159949759,-0.15976606450048,-0.548874290046456));
#10148=CARTESIAN_POINT('Ctrl Pts',(-0.820511285096538,-0.142345102874864,
-0.537715343527944));
#10149=CARTESIAN_POINT('Ctrl Pts',(-0.833661031856294,-0.0999305678883311,
-0.517157748491652));
#10150=CARTESIAN_POINT('Ctrl Pts',(-0.838633903678357,-0.0740444353928836,
-0.508899795931835));
#10151=CARTESIAN_POINT('Ctrl Pts',(-0.841298510752801,-0.04763,-0.504455939115715));
#10152=CARTESIAN_POINT('Origin',(-0.707106781186547,-0.04763,-0.707106781186548));
#10153=CARTESIAN_POINT('Origin',(0.,-0.04763,0.));
#10154=CARTESIAN_POINT('',(-0.238183666596899,-0.04763,-0.951592097314));
#10155=CARTESIAN_POINT('Origin',(0.,-0.04763,0.));
#10156=CARTESIAN_POINT('Origin',(5.55111512312578E-17,-0.04763,-1.));
#10157=CARTESIAN_POINT('Origin',(5.55111512312578E-17,0.,-1.));
#10158=CARTESIAN_POINT('',(0.238183666596899,-0.04763,-0.951592097314));
#10159=CARTESIAN_POINT('Ctrl Pts',(0.238183666596899,-0.04763,-0.951592097314));
#10160=CARTESIAN_POINT('Ctrl Pts',(0.233157223576062,-0.0740444353928835,
-0.952850216871763));
#10161=CARTESIAN_POINT('Ctrl Pts',(0.223801617934946,-0.099930567888331,
-0.955173119738174));
#10162=CARTESIAN_POINT('Ctrl Pts',(0.199966927975188,-0.142345102874864,
-0.960411259488514));
#10163=CARTESIAN_POINT('Ctrl Pts',(0.1868781821531,-0.15976606450048,-0.963103647174702));
#10164=CARTESIAN_POINT('Ctrl Pts',(0.15681442133453,-0.190326085855194,
-0.968453058988463));
#10165=CARTESIAN_POINT('Ctrl Pts',(0.139836317888042,-0.203463743702801,
-0.971100730005489));
#10166=CARTESIAN_POINT('Ctrl Pts',(0.104422493053067,-0.224161999508995,
-0.975530745318961));
#10167=CARTESIAN_POINT('Ctrl Pts',(0.0842175114474173,-0.232861760990032,
-0.977553872336861));
#10168=CARTESIAN_POINT('Ctrl Pts',(0.0421062857595698,-0.244251601209411,
-0.980270995488453));
#10169=CARTESIAN_POINT('Ctrl Pts',(0.0201990724523194,-0.246942143572133,
-0.980948));
#10170=CARTESIAN_POINT('Ctrl Pts',(-0.0201990724523193,-0.246942143572133,
-0.980948));
#10171=CARTESIAN_POINT('Ctrl Pts',(-0.0421062857595697,-0.244251601209411,
-0.980270995488453));
#10172=CARTESIAN_POINT('Ctrl Pts',(-0.0842175114474171,-0.232861760990032,
-0.977553872336861));
#10173=CARTESIAN_POINT('Ctrl Pts',(-0.104422493053067,-0.224161999508995,
-0.975530745318961));
#10174=CARTESIAN_POINT('Ctrl Pts',(-0.139836317888042,-0.203463743702801,
-0.971100730005489));
#10175=CARTESIAN_POINT('Ctrl Pts',(-0.15681442133453,-0.190326085855194,
-0.968453058988463));
#10176=CARTESIAN_POINT('Ctrl Pts',(-0.1868781821531,-0.15976606450048,-0.963103647174702));
#10177=CARTESIAN_POINT('Ctrl Pts',(-0.199966927975188,-0.142345102874864,
-0.960411259488514));
#10178=CARTESIAN_POINT('Ctrl Pts',(-0.223801617934945,-0.099930567888331,
-0.955173119738174));
#10179=CARTESIAN_POINT('Ctrl Pts',(-0.233157223576062,-0.0740444353928835,
-0.952850216871763));
#10180=CARTESIAN_POINT('Ctrl Pts',(-0.238183666596899,-0.0476299999999999,
-0.951592097314));
#10181=CARTESIAN_POINT('Origin',(5.55111512312578E-17,-0.04763,-1.));
#10182=CARTESIAN_POINT('Origin',(0.,-0.04763,0.));
#10183=CARTESIAN_POINT('',(0.504455939115715,-0.04763,-0.841298510752802));
#10184=CARTESIAN_POINT('Origin',(0.,-0.04763,0.));
#10185=CARTESIAN_POINT('Origin',(0.707106781186548,-0.04763,-0.707106781186547));
#10186=CARTESIAN_POINT('Origin',(0.707106781186548,0.,-0.707106781186547));
#10187=CARTESIAN_POINT('',(0.841298510752802,-0.04763,-0.504455939115715));
#10188=CARTESIAN_POINT('Ctrl Pts',(0.841298510752802,-0.04763,-0.504455939115715));
#10189=CARTESIAN_POINT('Ctrl Pts',(0.838633903678357,-0.0740444353928835,
-0.508899795931835));
#10190=CARTESIAN_POINT('Ctrl Pts',(0.833661031856294,-0.0999305678883309,
-0.517157748491652));
#10191=CARTESIAN_POINT('Ctrl Pts',(0.820511285096538,-0.142345102874864,
-0.537715343527944));
#10192=CARTESIAN_POINT('Ctrl Pts',(0.813159949759,-0.159766064500479,-0.548874290046456));
#10193=CARTESIAN_POINT('Ctrl Pts',(0.795684265985088,-0.190326085855194,
-0.573915184558107));
#10194=CARTESIAN_POINT('Ctrl Pts',(0.78555112003688,-0.203463743702801,
-0.587792702767295));
#10195=CARTESIAN_POINT('Ctrl Pts',(0.763642258217233,-0.224161999508995,
-0.615966552324775));
#10196=CARTESIAN_POINT('Ctrl Pts',(0.750785745543687,-0.232861760990032,
-0.631684198665438));
#10197=CARTESIAN_POINT('Ctrl Pts',(0.722929908501543,-0.244251601209411,
-0.663382628119203));
#10198=CARTESIAN_POINT('Ctrl Pts',(0.707917883896095,-0.246942143572133,
-0.679352081686668));
#10199=CARTESIAN_POINT('Ctrl Pts',(0.679352081686668,-0.246942143572133,
-0.707917883896095));
#10200=CARTESIAN_POINT('Ctrl Pts',(0.663382628119203,-0.244251601209411,
-0.722929908501543));
#10201=CARTESIAN_POINT('Ctrl Pts',(0.631684198665438,-0.232861760990032,
-0.750785745543687));
#10202=CARTESIAN_POINT('Ctrl Pts',(0.615966552324775,-0.224161999508995,
-0.763642258217232));
#10203=CARTESIAN_POINT('Ctrl Pts',(0.587792702767295,-0.203463743702801,
-0.78555112003688));
#10204=CARTESIAN_POINT('Ctrl Pts',(0.573915184558107,-0.190326085855194,
-0.795684265985088));
#10205=CARTESIAN_POINT('Ctrl Pts',(0.548874290046456,-0.159766064500479,
-0.813159949759));
#10206=CARTESIAN_POINT('Ctrl Pts',(0.537715343527944,-0.142345102874864,
-0.820511285096538));
#10207=CARTESIAN_POINT('Ctrl Pts',(0.517157748491652,-0.099930567888331,
-0.833661031856294));
#10208=CARTESIAN_POINT('Ctrl Pts',(0.508899795931835,-0.0740444353928835,
-0.838633903678357));
#10209=CARTESIAN_POINT('Ctrl Pts',(0.504455939115715,-0.04763,-0.841298510752801));
#10210=CARTESIAN_POINT('Origin',(0.707106781186548,-0.04763,-0.707106781186547));
#10211=CARTESIAN_POINT('Origin',(0.,-0.166705,0.));
#10212=CARTESIAN_POINT('',(-0.980948,-0.28578,1.20131482833E-16));
#10213=CARTESIAN_POINT('Origin',(0.,-0.28578,0.));
#10214=CARTESIAN_POINT('',(-0.980948,-0.166705,1.20131482833E-16));
#10215=CARTESIAN_POINT('',(0.951592097314,-0.04763,0.238183666596899));
#10216=CARTESIAN_POINT('Origin',(0.,-0.04763,0.));
#10217=CARTESIAN_POINT('',(0.951592097314,-0.04763,-0.238183666596899));
#10218=CARTESIAN_POINT('Ctrl Pts',(0.951592097314,-0.04763,0.238183666596899));
#10219=CARTESIAN_POINT('Ctrl Pts',(0.952850216871763,-0.0740444353928835,
0.233157223576062));
#10220=CARTESIAN_POINT('Ctrl Pts',(0.955173119738174,-0.099930567888331,
0.223801617934945));
#10221=CARTESIAN_POINT('Ctrl Pts',(0.960411259488514,-0.142345102874864,
0.199966927975188));
#10222=CARTESIAN_POINT('Ctrl Pts',(0.963103647174702,-0.15976606450048,
0.1868781821531));
#10223=CARTESIAN_POINT('Ctrl Pts',(0.968453058988463,-0.190326085855194,
0.15681442133453));
#10224=CARTESIAN_POINT('Ctrl Pts',(0.971100730005489,-0.203463743702801,
0.139836317888042));
#10225=CARTESIAN_POINT('Ctrl Pts',(0.975530745318961,-0.224161999508995,
0.104422493053067));
#10226=CARTESIAN_POINT('Ctrl Pts',(0.977553872336861,-0.232861760990032,
0.0842175114474172));
#10227=CARTESIAN_POINT('Ctrl Pts',(0.980270995488453,-0.244251601209411,
0.0421062857595697));
#10228=CARTESIAN_POINT('Ctrl Pts',(0.980948,-0.246942143572133,0.0201990724523194));
#10229=CARTESIAN_POINT('Ctrl Pts',(0.980948,-0.246942143572133,-0.0201990724523194));
#10230=CARTESIAN_POINT('Ctrl Pts',(0.980270995488453,-0.244251601209411,
-0.0421062857595697));
#10231=CARTESIAN_POINT('Ctrl Pts',(0.977553872336861,-0.232861760990032,
-0.0842175114474172));
#10232=CARTESIAN_POINT('Ctrl Pts',(0.975530745318961,-0.224161999508995,
-0.104422493053067));
#10233=CARTESIAN_POINT('Ctrl Pts',(0.971100730005489,-0.203463743702801,
-0.139836317888042));
#10234=CARTESIAN_POINT('Ctrl Pts',(0.968453058988463,-0.190326085855194,
-0.15681442133453));
#10235=CARTESIAN_POINT('Ctrl Pts',(0.963103647174702,-0.15976606450048,
-0.1868781821531));
#10236=CARTESIAN_POINT('Ctrl Pts',(0.960411259488514,-0.142345102874864,
-0.199966927975188));
#10237=CARTESIAN_POINT('Ctrl Pts',(0.955173119738174,-0.099930567888331,
-0.223801617934945));
#10238=CARTESIAN_POINT('Ctrl Pts',(0.952850216871763,-0.0740444353928835,
-0.233157223576062));
#10239=CARTESIAN_POINT('Ctrl Pts',(0.951592097314,-0.0476299999999999,-0.238183666596899));
#10240=CARTESIAN_POINT('Origin',(0.,-0.04763,0.));
#10241=CARTESIAN_POINT('Origin',(0.,-0.04763,0.));
#10242=CARTESIAN_POINT('Origin',(1.,-0.04763,0.));
#10243=CARTESIAN_POINT('Origin',(1.,0.,0.));
#10244=CARTESIAN_POINT('Origin',(1.,-0.04763,0.));
#10245=CARTESIAN_POINT('Origin',(0.,-0.28578,0.));
#10246=CARTESIAN_POINT('Origin',(0.,-0.04763,0.));
#10465=UNCERTAINTY_MEASURE_WITH_UNIT(LENGTH_MEASURE(0.001),#10511,
'DISTANCE_ACCURACY_VALUE',
'Maximum model space distance between geometric entities at asserted c
onnectivities');
#10471=UNCERTAINTY_MEASURE_WITH_UNIT(LENGTH_MEASURE(0.001),#10511,
'DISTANCE_ACCURACY_VALUE',
'Maximum model space distance between geometric entities at asserted c
onnectivities');
#10504=(
GEOMETRIC_REPRESENTATION_CONTEXT(3)
GLOBAL_UNCERTAINTY_ASSIGNED_CONTEXT((#10465))
GLOBAL_UNIT_ASSIGNED_CONTEXT((#10511,#10513,#10514))
REPRESENTATION_CONTEXT('','3D')
);
#10510=(
GEOMETRIC_REPRESENTATION_CONTEXT(3)
GLOBAL_UNCERTAINTY_ASSIGNED_CONTEXT((#10471))
GLOBAL_UNIT_ASSIGNED_CONTEXT((#10511,#10513,#10514))
REPRESENTATION_CONTEXT('','3D')
);
#10511=(
LENGTH_UNIT()
NAMED_UNIT(*)
SI_UNIT(.CENTI.,.METRE.)
);
#10513=(
NAMED_UNIT(*)
PLANE_ANGLE_UNIT()
SI_UNIT($,.RADIAN.)
);
#10514=(
NAMED_UNIT(*)
SI_UNIT($,.STERADIAN.)
SOLID_ANGLE_UNIT()
);
#10547=SHAPE_DEFINITION_REPRESENTATION(#10590,#10677);
#10590=PRODUCT_DEFINITION_SHAPE('',$,#10716);
#10677=SHAPE_REPRESENTATION('',(#6250),#10504);
#10683=PRODUCT_DEFINITION_CONTEXT('part definition',#10799,'design');
#10716=PRODUCT_DEFINITION('Cage (1)','Cage (1)',#10754,#10683);
#10754=PRODUCT_DEFINITION_FORMATION('',$,#10833);
#10799=APPLICATION_CONTEXT(
'Core Data for Automotive Mechanical Design Process');
#10800=PRODUCT_CONTEXT('part definition',#10799,'mechanical');
#10833=PRODUCT('Cage (1)','Cage (1)','Cage (1)',(#10800));
#10902=COLOUR_RGB('Grey',0.48,0.52,0.57);
#10903=FILL_AREA_STYLE_COLOUR('',#10902);
#10904=FILL_AREA_STYLE('',(#10903));
#10905=SURFACE_STYLE_FILL_AREA(#10904);
#10906=SURFACE_SIDE_STYLE('',(#10905));
#10907=SURFACE_STYLE_USAGE(.BOTH.,#10906);
#10908=PRESENTATION_STYLE_ASSIGNMENT((#10907));
ENDSEC;
END-ISO-10303-21;
